ISO-10303-21;
HEADER;
/* Generated by software containing ST-Developer
 * from STEP Tools, Inc. (www.steptools.com) 
 */

FILE_DESCRIPTION(
/* description */ (''),
/* implementation_level */ '2;1');

FILE_NAME(
/* name */ 'Nut.step',
/* time_stamp */ '2026-10-05T15:35:09-07:00',
/* author */ (''),
/* organization */ (''),
/* preprocessor_version */ 'ST-DEVELOPER v20.2',
/* originating_system */ 'Autodesk Translation Framework v15.15.0.0',
/* authorisation */ '');

FILE_SCHEMA (('AUTOMOTIVE_DESIGN { 1 0 10303 214 3 1 1 }'));
ENDSEC;

DATA;
#10=MECHANICAL_DESIGN_GEOMETRIC_PRESENTATION_REPRESENTATION('',(#549),#74523);
#47=ELLIPSE('',#5049,4.99855036794194,3.19830998796427);
#48=B_SPLINE_SURFACE_WITH_KNOTS('',3,3,((#6899,#6900,#6901,#6902,#6903,
#6904,#6905,#6906,#6907,#6908,#6909,#6910,#6911,#6912,#6913,#6914,#6915,
#6916,#6917,#6918,#6919,#6920,#6921,#6922,#6923,#6924,#6925,#6926,#6927,
#6928,#6929),(#6930,#6931,#6932,#6933,#6934,#6935,#6936,#6937,#6938,#6939,
#6940,#6941,#6942,#6943,#6944,#6945,#6946,#6947,#6948,#6949,#6950,#6951,
#6952,#6953,#6954,#6955,#6956,#6957,#6958,#6959,#6960),(#6961,#6962,#6963,
#6964,#6965,#6966,#6967,#6968,#6969,#6970,#6971,#6972,#6973,#6974,#6975,
#6976,#6977,#6978,#6979,#6980,#6981,#6982,#6983,#6984,#6985,#6986,#6987,
#6988,#6989,#6990,#6991),(#6992,#6993,#6994,#6995,#6996,#6997,#6998,#6999,
#7000,#7001,#7002,#7003,#7004,#7005,#7006,#7007,#7008,#7009,#7010,#7011,
#7012,#7013,#7014,#7015,#7016,#7017,#7018,#7019,#7020,#7021,#7022)),
 .UNSPECIFIED.,.F.,.F.,.F.,(4,4),(4,1,1,1,1,1,1,1,1,1,1,1,1,1,1,1,1,1,1,
1,1,1,1,1,1,1,1,1,4),(-4.22102652940044E-5,0.112813165026554),(14.3984001269721,
14.8716759259636,15.344951724955,15.8182275239465,16.2915033229379,16.7647791219294,
17.2380549209208,17.7113307199123,18.1846065189038,18.6578823178952,19.1311581168867,
19.6044339158781,20.0777097148696,20.5509855138611,21.0242613128525,21.497537111844,
21.9708129108354,22.4440887098269,22.9173645088184,23.3906403078098,23.8639161068013,
24.3371919057927,24.8104677047842,25.2837435037757,25.7570193027671,26.2302951017586,
26.70357090075,27.1768466997415,27.6501791561868),.UNSPECIFIED.);
#49=B_SPLINE_SURFACE_WITH_KNOTS('',3,3,((#7342,#7343,#7344,#7345,#7346,
#7347,#7348,#7349,#7350,#7351,#7352,#7353,#7354,#7355,#7356,#7357,#7358,
#7359,#7360,#7361,#7362,#7363,#7364,#7365,#7366,#7367,#7368,#7369,#7370),
(#7371,#7372,#7373,#7374,#7375,#7376,#7377,#7378,#7379,#7380,#7381,#7382,
#7383,#7384,#7385,#7386,#7387,#7388,#7389,#7390,#7391,#7392,#7393,#7394,
#7395,#7396,#7397,#7398,#7399),(#7400,#7401,#7402,#7403,#7404,#7405,#7406,
#7407,#7408,#7409,#7410,#7411,#7412,#7413,#7414,#7415,#7416,#7417,#7418,
#7419,#7420,#7421,#7422,#7423,#7424,#7425,#7426,#7427,#7428),(#7429,#7430,
#7431,#7432,#7433,#7434,#7435,#7436,#7437,#7438,#7439,#7440,#7441,#7442,
#7443,#7444,#7445,#7446,#7447,#7448,#7449,#7450,#7451,#7452,#7453,#7454,
#7455,#7456,#7457)),.UNSPECIFIED.,.F.,.F.,.F.,(4,4),(4,1,1,1,1,1,1,1,1,
1,1,1,1,1,1,1,1,1,1,1,1,1,1,1,1,1,4),(-6.68859175462372E-5,0.112808473639489),
(11.8516667789337,12.3448673159975,12.8380009671439,13.3311346182902,13.8242682694366,
14.3174019205829,14.8105355717293,15.3036692228756,15.796802874022,16.2899365251684,
16.7830701763147,17.2762038274611,17.7693374786074,18.2624711297538,18.7556047809001,
19.2487384320465,19.7418720831929,20.2350057343392,20.7281393854856,21.2212730366319,
21.7144066877783,22.2075403389246,22.700673990071,23.1938076412174,23.6869412923637,
24.1800749435101,24.6732085946564),.UNSPECIFIED.);
#50=B_SPLINE_SURFACE_WITH_KNOTS('',3,3,((#7678,#7679,#7680,#7681,#7682,
#7683,#7684),(#7685,#7686,#7687,#7688,#7689,#7690,#7691),(#7692,#7693,#7694,
#7695,#7696,#7697,#7698),(#7699,#7700,#7701,#7702,#7703,#7704,#7705)),
 .UNSPECIFIED.,.F.,.F.,.F.,(4,4),(4,1,1,1,4),(-3.56765467420186E-5,0.112774496143046),
(25.715772779332,26.1650876565626,26.614384545223,27.0636814338833,27.512996311114),
 .UNSPECIFIED.);
#51=B_SPLINE_SURFACE_WITH_KNOTS('',3,3,((#7757,#7758,#7759,#7760,#7761),
(#7762,#7763,#7764,#7765,#7766),(#7767,#7768,#7769,#7770,#7771),(#7772,
#7773,#7774,#7775,#7776)),.UNSPECIFIED.,.F.,.F.,.F.,(4,4),(4,1,4),(0.0695195007674178,
0.112756507572734),(29.185865369981,29.6029901263762,30.1591564682366),
 .UNSPECIFIED.);
#52=B_SPLINE_SURFACE_WITH_KNOTS('',3,3,((#7783,#7784,#7785,#7786,#7787),
(#7788,#7789,#7790,#7791,#7792),(#7793,#7794,#7795,#7796,#7797),(#7798,
#7799,#7800,#7801,#7802)),.UNSPECIFIED.,.F.,.F.,.F.,(4,4),(4,1,4),(0.,0.113001416241296),
(29.1062173671441,29.7730867005616,30.4397111253108),.UNSPECIFIED.);
#60=B_SPLINE_CURVE_WITH_KNOTS('',3,(#6462,#6463,#6464,#6465),
 .UNSPECIFIED.,.F.,.F.,(4,4),(24.2167824327583,24.6732085946564),
 .UNSPECIFIED.);
#61=B_SPLINE_CURVE_WITH_KNOTS('',3,(#6467,#6468,#6469,#6470,#6471,#6472),
 .UNSPECIFIED.,.F.,.F.,(4,2,4),(-0.753063156930721,-0.748287180828045,-0.713936115042439),
 .UNSPECIFIED.);
#62=B_SPLINE_CURVE_WITH_KNOTS('',3,(#6473,#6474,#6475,#6476,#6477,#6478,
#6479,#6480),.UNSPECIFIED.,.F.,.F.,(4,2,2,4),(7.54703642806723E-5,0.0982305326102068,
0.1956130339559,0.318929227615191),.UNSPECIFIED.);
#63=B_SPLINE_CURVE_WITH_KNOTS('',3,(#6486,#6487,#6488,#6489,#6490,#6491,
#6492,#6493,#6494,#6495,#6496,#6497,#6498,#6499,#6500,#6501,#6502,#6503,
#6504,#6505,#6506,#6507),.UNSPECIFIED.,.F.,.F.,(4,2,2,2,2,2,2,2,2,2,4),
(4.17196893903895,4.31793438390998,4.49439067838144,4.61169587925562,4.80346275986459,
4.92105347661489,5.03845115754435,5.15675731126169,5.34520640965897,5.44042607659759,
5.5359732292178),.UNSPECIFIED.);
#64=B_SPLINE_CURVE_WITH_KNOTS('',3,(#6509,#6510,#6511,#6512,#6513,#6514),
 .UNSPECIFIED.,.F.,.F.,(4,1,1,4),(14.3984001269721,14.8716759259636,15.344951724955,
15.707963267949),.UNSPECIFIED.);
#65=B_SPLINE_CURVE_WITH_KNOTS('',3,(#6517,#6518,#6519,#6520,#6521,#6522,
#6523,#6524,#6525,#6526,#6527,#6528,#6529,#6530,#6531,#6532,#6533,#6534,
#6535,#6536,#6537,#6538,#6539,#6540,#6541,#6542,#6543,#6544,#6545,#6546,
#6547,#6548,#6549,#6550,#6551,#6552,#6553,#6554),.UNSPECIFIED.,.F.,.F.,
(4,2,2,2,2,2,2,2,2,2,2,2,2,2,2,2,2,2,4),(8.93612119710033E-5,0.137519605080263,
0.271503523144846,0.360853537619444,0.59605291228506,0.714174537685151,
0.86920957112301,0.986431819009906,1.16462578939155,1.28180463200857,1.46548324524592,
1.58267186650919,1.82234561940174,1.9411521807847,2.05786559772135,2.17524669758369,
2.36994176720202,2.48715613899137,2.4871743415165),.UNSPECIFIED.);
#66=B_SPLINE_CURVE_WITH_KNOTS('',3,(#6560,#6561,#6562,#6563,#6564,#6565,
#6566,#6567,#6568,#6569,#6570,#6571,#6572,#6573,#6574,#6575,#6576,#6577,
#6578,#6579,#6580,#6581,#6582,#6583,#6584,#6585,#6586,#6587,#6588,#6589,
#6590,#6591,#6592,#6593,#6594,#6595,#6596,#6597),.UNSPECIFIED.,.F.,.F.,
(4,2,2,2,2,2,2,2,2,2,2,2,2,2,2,2,2,2,4),(3.44081285251957E-5,0.12033556566363,
0.23797701963383,0.316579069165278,0.52134934559798,0.620831783340204,0.72063091120251,
0.82039841485169,1.02523503080041,1.12459939419803,1.2245754078634,1.42416968131716,
1.52608431165409,1.62528028417853,1.72551932408833,1.92432671834024,2.02032569726045,
2.11939118662542,2.17146271467381),.UNSPECIFIED.);
#67=B_SPLINE_CURVE_WITH_KNOTS('',3,(#6600,#6601,#6602,#6603,#6604,#6605,
#6606,#6607,#6608,#6609,#6610,#6611,#6612,#6613,#6614,#6615,#6616,#6617,
#6618,#6619,#6620,#6621,#6622,#6623,#6624,#6625,#6626,#6627,#6628,#6629,
#6630,#6631,#6632,#6633,#6634,#6635,#6636,#6637,#6638,#6639,#6640,#6641,
#6642,#6643,#6644,#6645,#6646,#6647,#6648,#6649,#6650,#6651),
 .UNSPECIFIED.,.F.,.F.,(4,2,2,2,2,2,2,2,2,2,2,2,2,2,2,2,2,2,2,2,2,2,2,2,
2,4),(-5.78791727609175,-5.60765656906696,-5.54795034782102,-5.34916073937174,
-5.29912888856794,-5.09895513119324,-4.99903636368212,-4.90018494634977,
-4.80099712110515,-4.64008086509064,-4.54087127009457,-4.44071265045858,
-4.24069819901497,-4.13871795375788,-4.08861417004609,-3.89168204538907,
-3.8416016546448,-3.64330286264328,-3.59325472626477,-3.39352696698553,
-3.29366130100268,-3.19468247312873,-3.09545501998428,-2.89395588410736,
-2.79440271848196,-2.7332430357663),.UNSPECIFIED.);
#68=B_SPLINE_CURVE_WITH_KNOTS('',3,(#6654,#6655,#6656,#6657,#6658,#6659,
#6660,#6661,#6662,#6663,#6664,#6665,#6666,#6667,#6668,#6669,#6670,#6671,
#6672,#6673,#6674,#6675,#6676,#6677,#6678,#6679,#6680,#6681,#6682,#6683,
#6684,#6685,#6686,#6687,#6688,#6689,#6690,#6691,#6692,#6693,#6694,#6695,
#6696,#6697,#6698,#6699),.UNSPECIFIED.,.F.,.F.,(4,2,2,2,2,2,2,2,2,2,2,2,
2,2,2,2,2,2,2,2,2,2,4),(-2.7332430357663,-2.69484018883808,-2.50140826620732,
-2.45132601081293,-2.25469999769462,-2.20459657737961,-2.10261367763625,
-1.90262055882343,-1.7012130032506,-1.53229381391829,-1.43289581954836,
-1.33349729581112,-1.23385688191433,-1.03631520063649,-0.986225259842964,
-0.796325042864855,-0.746270935737797,-0.548519362328493,-0.498429295003538,
-0.308427409772446,-0.231816757097687,-0.117078636027805,-2.91462933559131E-5),
 .UNSPECIFIED.);
#69=B_SPLINE_CURVE_WITH_KNOTS('',3,(#6701,#6702,#6703,#6704,#6705,#6706),
 .UNSPECIFIED.,.F.,.F.,(4,2,4),(0.990341797688948,1.00950965231655,1.12413598826008),
 .UNSPECIFIED.);
#70=B_SPLINE_CURVE_WITH_KNOTS('',3,(#6707,#6708,#6709,#6710,#6711,#6712,
#6713,#6714,#6715,#6716,#6717,#6718,#6719,#6720,#6721,#6722,#6723,#6724,
#6725,#6726,#6727,#6728,#6729,#6730,#6731,#6732,#6733,#6734,#6735,#6736,
#6737,#6738,#6739,#6740,#6741,#6742,#6743,#6744,#6745,#6746,#6747,#6748,
#6749,#6750),.UNSPECIFIED.,.F.,.F.,(4,2,2,2,2,2,2,2,2,2,2,2,2,2,2,2,2,2,
2,2,2,4),(2.17146271467381,2.32081873718431,2.42085332522106,2.51962847719786,
2.71909167222752,2.81827420130679,2.91707565944408,3.01709099728558,3.21846106537803,
3.31753071425488,3.41512303096382,3.61371567918643,3.81514697300165,3.9170831998352,
4.11631543055948,4.21640643470696,4.3157013669682,4.52051919296804,4.72221203817467,
4.87879648597379,4.95931330752704,5.04024048342652),.UNSPECIFIED.);
#71=B_SPLINE_CURVE_WITH_KNOTS('',3,(#6753,#6754,#6755,#6756,#6757,#6758,
#6759,#6760,#6761,#6762,#6763,#6764,#6765,#6766,#6767,#6768,#6769,#6770,
#6771,#6772,#6773,#6774,#6775,#6776,#6777,#6778,#6779,#6780,#6781,#6782,
#6783,#6784,#6785,#6786),.UNSPECIFIED.,.F.,.F.,(4,2,2,2,2,2,2,2,2,2,2,2,
2,2,2,2,4),(2.4871743415165,2.7262469977791,2.84376601052792,2.96216019071238,
3.19950395965916,3.31681308535098,3.43325766283811,3.55221021297849,3.7923702493438,
3.90957368072485,4.08096889312944,4.19841225295174,4.34417466823886,4.46297946676196,
4.70267246641313,4.83714481429229,4.97526148947484),.UNSPECIFIED.);
#72=B_SPLINE_CURVE_WITH_KNOTS('',3,(#6787,#6788,#6789,#6790,#6791,#6792,
#6793,#6794,#6795),.UNSPECIFIED.,.F.,.F.,(4,1,1,1,1,1,4),(21.9911485915565,
22.2075403389246,22.700673990071,23.1938076412174,23.6869412923637,24.1800749435101,
24.2167824327583),.UNSPECIFIED.);
#73=B_SPLINE_CURVE_WITH_KNOTS('',3,(#6796,#6797,#6798,#6799,#6800,#6801,
#6802,#6803,#6804,#6805,#6806,#6807,#6808,#6809,#6810,#6811,#6812,#6813,
#6814,#6815,#6816,#6817,#6818,#6819,#6820,#6821,#6822,#6823,#6824,#6825,
#6826,#6827,#6828,#6829,#6830,#6831,#6832,#6833,#6834,#6835,#6836,#6837,
#6838,#6839,#6840,#6841,#6842,#6843,#6844,#6845,#6846,#6847,#6848,#6849),
 .UNSPECIFIED.,.F.,.F.,(4,2,2,2,2,2,2,2,2,2,2,2,2,2,2,2,2,2,2,2,2,2,2,2,
2,2,4),(0.318929227615191,0.384926038912769,0.502349680213896,0.619949001797926,
0.858373875895787,0.977114949500405,1.09371003157623,1.21105237421161,1.45123133000857,
1.57041674209182,1.69164385601961,1.80907474394577,2.04918305373556,2.29265580161209,
2.41076173271125,2.52856060749483,2.76820125234305,2.88569212998167,3.00282499176873,
3.1212892898508,3.35779947665438,3.41724850868636,3.6606559769089,3.72024554799103,
3.84139057999963,4.07822973147708,4.17196893903895),.UNSPECIFIED.);
#74=B_SPLINE_CURVE_WITH_KNOTS('',3,(#6856,#6857,#6858,#6859,#6860,#6861,
#6862,#6863,#6864,#6865,#6866,#6867,#6868,#6869,#6870,#6871,#6872,#6873,
#6874,#6875,#6876,#6877,#6878,#6879,#6880,#6881,#6882,#6883,#6884,#6885,
#6886,#6887,#6888,#6889,#6890,#6891,#6892,#6893,#6894,#6895,#6896,#6897,
#6898),.UNSPECIFIED.,.F.,.F.,(4,3,3,3,3,3,3,3,3,3,3,3,3,3,4),(-1.14369947197745,
-1.09266156206797,-1.04162734604678,-1.01275777609579,-0.99955287370654,
-0.991008573822155,-0.940790330265059,-0.890909857971607,-0.870850090088419,
-0.859711737003807,-0.8511853223161,-0.810670786438855,-0.761368249661256,
-0.712264686030117,-0.682622141321854),.UNSPECIFIED.);
#75=B_SPLINE_CURVE_WITH_KNOTS('',3,(#7024,#7025,#7026,#7027,#7028,#7029,
#7030,#7031,#7032,#7033,#7034,#7035,#7036,#7037,#7038,#7039,#7040,#7041,
#7042,#7043,#7044,#7045,#7046,#7047,#7048,#7049),.UNSPECIFIED.,.F.,.F.,
(4,2,2,2,2,2,2,2,2,2,2,2,4),(-0.514016614331628,-0.32969130617147,-0.294713516998778,
-0.279199880107329,-0.271856778418491,-0.268695348946667,-0.266392385760583,
-0.264283697040262,-0.261451067661434,-0.254187829707465,-0.238561902747748,
-0.203303015946135,-1.727286035542E-5),.UNSPECIFIED.);
#76=B_SPLINE_CURVE_WITH_KNOTS('',3,(#7051,#7052,#7053,#7054,#7055,#7056,
#7057,#7058,#7059,#7060,#7061,#7062,#7063,#7064,#7065,#7066,#7067,#7068,
#7069,#7070,#7071,#7072,#7073,#7074,#7075,#7076,#7077,#7078,#7079,#7080,
#7081,#7082,#7083,#7084,#7085,#7086,#7087,#7088,#7089,#7090,#7091,#7092,
#7093,#7094,#7095,#7096,#7097,#7098,#7099,#7100,#7101,#7102,#7103,#7104,
#7105,#7106,#7107,#7108,#7109,#7110,#7111,#7112,#7113,#7114,#7115,#7116,
#7117,#7118,#7119,#7120,#7121,#7122,#7123,#7124,#7125,#7126),
 .UNSPECIFIED.,.F.,.F.,(4,3,3,3,3,3,3,3,3,3,3,3,3,3,3,3,3,3,3,3,3,3,3,3,
3,4),(25.6488293377177,25.7363230860383,25.7570193027671,25.8403521785318,
25.9236708927411,26.006992682315,26.0903100076079,26.1736446045009,26.2302951017586,
26.3136869261066,26.397064749755,26.4804453409533,26.5638211615191,26.6472132739149,
26.70357090075,26.786786729163,26.869987834458,26.953192221565,27.0363925108091,
27.119611617046,27.1768466997415,27.2602763642278,27.3436962816524,27.4271047300443,
27.5105172922409,27.557778459707),.UNSPECIFIED.);
#77=B_SPLINE_CURVE_WITH_KNOTS('',3,(#7127,#7128,#7129,#7130,#7131,#7132),
 .UNSPECIFIED.,.F.,.F.,(4,2,4),(-0.123598918531262,-0.0618193643105504,
0.),.UNSPECIFIED.);
#78=B_SPLINE_CURVE_WITH_KNOTS('',3,(#7133,#7134,#7135,#7136,#7137,#7138,
#7139,#7140,#7141,#7142,#7143,#7144,#7145,#7146,#7147,#7148,#7149,#7150,
#7151,#7152,#7153,#7154,#7155,#7156,#7157,#7158,#7159,#7160,#7161,#7162,
#7163,#7164,#7165,#7166,#7167,#7168,#7169,#7170,#7171,#7172,#7173,#7174,
#7175,#7176,#7177,#7178,#7179,#7180,#7181,#7182,#7183,#7184,#7185,#7186,
#7187,#7188,#7189,#7190,#7191,#7192,#7193,#7194,#7195,#7196,#7197,#7198,
#7199,#7200,#7201,#7202,#7203,#7204,#7205,#7206,#7207,#7208,#7209,#7210,
#7211,#7212,#7213,#7214,#7215,#7216,#7217,#7218,#7219,#7220,#7221,#7222,
#7223,#7224,#7225,#7226,#7227,#7228,#7229,#7230,#7231,#7232,#7233,#7234,
#7235,#7236,#7237,#7238),.UNSPECIFIED.,.F.,.F.,(4,3,3,3,3,3,3,3,3,3,3,3,
3,3,3,3,3,3,3,3,3,3,3,3,3,3,3,3,3,3,3,3,3,3,3,4),(1.32259959060234E-14,
0.050745690367541,0.101728144589328,0.152317867535398,0.202221298354011,
0.223115699003081,0.233292020958922,0.239422790003241,0.28579890095029,
0.335558319036143,0.385169128031006,0.429266865985378,0.448104138024905,
0.458259185053611,0.466209278741972,0.514659008147364,0.561141261429649,
0.609757592303607,0.657860913002203,0.682148882539776,0.688028355480578,
0.735403736851129,0.782365796754906,0.825913733428173,0.873065043083829,
0.888022019180938,0.895029710778973,0.9017703672553,0.948154249761794,0.994183679961664,
1.0163582276839,1.02409536336603,1.06944623508431,1.07956252253316,1.12521097349135,
1.14790980755862),.UNSPECIFIED.);
#79=B_SPLINE_CURVE_WITH_KNOTS('',3,(#7241,#7242,#7243,#7244),
 .UNSPECIFIED.,.F.,.F.,(4,4),(-2.53462644400385,-2.50471137450691),
 .UNSPECIFIED.);
#80=B_SPLINE_CURVE_WITH_KNOTS('',3,(#7246,#7247,#7248,#7249),
 .UNSPECIFIED.,.F.,.F.,(4,4),(-1.34654518817506,-1.30462978372618),
 .UNSPECIFIED.);
#81=B_SPLINE_CURVE_WITH_KNOTS('',3,(#7250,#7251,#7252,#7253,#7254,#7255,
#7256,#7257,#7258,#7259,#7260,#7261,#7262,#7263,#7264,#7265,#7266,#7267,
#7268,#7269,#7270,#7271,#7272,#7273,#7274,#7275,#7276,#7277,#7278,#7279,
#7280,#7281,#7282,#7283,#7284,#7285,#7286,#7287,#7288,#7289,#7290,#7291,
#7292,#7293,#7294,#7295,#7296,#7297,#7298,#7299,#7300,#7301,#7302,#7303,
#7304,#7305,#7306,#7307,#7308,#7309,#7310,#7311,#7312,#7313,#7314,#7315,
#7316,#7317,#7318,#7319,#7320,#7321,#7322),.UNSPECIFIED.,.F.,.F.,(4,3,3,
3,3,3,3,3,3,3,3,3,3,3,3,3,3,3,3,3,3,3,3,3,4),(25.7157907679023,25.7998921857034,
25.8839886324584,25.9680923853322,26.0521932755846,26.1363032915209,26.1650876565626,
26.2484227066867,26.3317477086458,26.4150799956916,26.4984115627295,26.5817614677887,
26.614384545223,26.6977343289403,26.781067684511,26.8643988612109,26.9477238552507,
27.0310591851449,27.0636814338833,27.1477914052286,27.2318926685899,27.3159957185016,
27.4000927043931,27.4841941803579,27.5129783225437),.UNSPECIFIED.);
#82=B_SPLINE_CURVE_WITH_KNOTS('',3,(#7327,#7328,#7329,#7330,#7331),
 .UNSPECIFIED.,.F.,.F.,(4,1,4),(29.135142171349,29.7730867005616,30.4397111253108),
 .UNSPECIFIED.);
#83=B_SPLINE_CURVE_WITH_KNOTS('',3,(#7333,#7334,#7335,#7336),
 .UNSPECIFIED.,.F.,.F.,(4,4),(-3.54732626370964,-3.51350080410364),
 .UNSPECIFIED.);
#84=B_SPLINE_CURVE_WITH_KNOTS('',3,(#7337,#7338,#7339,#7340,#7341),
 .UNSPECIFIED.,.F.,.F.,(4,1,4),(29.185865369981,29.6029901263762,30.1591564682366),
 .UNSPECIFIED.);
#85=B_SPLINE_CURVE_WITH_KNOTS('',3,(#7459,#7460,#7461,#7462,#7463,#7464),
 .UNSPECIFIED.,.F.,.F.,(4,2,4),(-0.220733411845382,-0.110386618861819,-4.77244559407116E-5),
 .UNSPECIFIED.);
#86=B_SPLINE_CURVE_WITH_KNOTS('',3,(#7465,#7466,#7467,#7468,#7469,#7470,
#7471,#7472,#7473,#7474,#7475,#7476,#7477,#7478,#7479,#7480,#7481,#7482,
#7483,#7484,#7485,#7486,#7487,#7488,#7489,#7490,#7491,#7492,#7493,#7494,
#7495,#7496,#7497,#7498,#7499,#7500,#7501,#7502,#7503,#7504,#7505,#7506,
#7507,#7508,#7509,#7510,#7511,#7512,#7513,#7514,#7515,#7516,#7517,#7518,
#7519,#7520,#7521,#7522,#7523,#7524,#7525,#7526,#7527,#7528,#7529,#7530,
#7531,#7532,#7533,#7534,#7535,#7536,#7537,#7538,#7539,#7540,#7541,#7542,
#7543,#7544,#7545,#7546,#7547,#7548,#7549,#7550,#7551,#7552,#7553,#7554,
#7555,#7556,#7557,#7558,#7559,#7560,#7561,#7562,#7563,#7564,#7565,#7566,
#7567,#7568,#7569,#7570,#7571,#7572,#7573,#7574,#7575,#7576,#7577,#7578,
#7579),.UNSPECIFIED.,.F.,.F.,(4,3,3,3,3,3,3,3,3,3,3,3,3,3,3,3,3,3,3,3,3,
3,3,3,3,3,3,3,3,3,3,3,3,3,3,3,3,3,4),(7.86929992325189E-14,0.0451936811860495,
0.0903969215350478,0.136144750154152,0.180774724743962,0.192656156822049,
0.202437724302502,0.208102574890687,0.254797163791912,0.260907252703528,
0.307156117174411,0.353882768105037,0.400800570233627,0.407990886645808,
0.414297194758911,0.462166258294729,0.510035321830547,0.533410739071612,
0.581324090737381,0.610800619774486,0.624309700326862,0.630783725208717,
0.637288545122989,0.686044941542277,0.735263135531318,0.784542352881166,
0.81734010039149,0.836777243703415,0.85029153110938,0.857044629992751,0.907491336547556,
0.957938043102361,0.980210958730824,0.997207592144651,1.00463770128361,
1.05568876682972,1.10658093101247,1.11216107549305,1.14369466111386),
 .UNSPECIFIED.);
#87=B_SPLINE_CURVE_WITH_KNOTS('',3,(#7581,#7582,#7583,#7584,#7585,#7586,
#7587,#7588,#7589,#7590,#7591,#7592,#7593,#7594,#7595,#7596,#7597,#7598,
#7599,#7600,#7601,#7602,#7603,#7604,#7605,#7606,#7607,#7608,#7609,#7610),
 .UNSPECIFIED.,.F.,.F.,(4,2,2,2,2,2,2,2,2,2,2,2,2,2,4),(-0.515686766343526,
-0.398525158108789,-0.320476105936825,-0.276727278366829,-0.257809834269005,
-0.25033771712097,-0.246969508664653,-0.244560940095557,-0.242057971080847,
-0.238341190453125,-0.228151135260896,-0.205623012766941,-0.150948653470694,
-0.0744708908354928,0.),.UNSPECIFIED.);
#88=B_SPLINE_CURVE_WITH_KNOTS('',3,(#7611,#7612,#7613,#7614,#7615,#7616,
#7617,#7618,#7619,#7620,#7621,#7622,#7623,#7624,#7625,#7626,#7627,#7628,
#7629,#7630,#7631,#7632,#7633,#7634,#7635,#7636,#7637,#7638,#7639,#7640,
#7641,#7642,#7643,#7644,#7645,#7646,#7647,#7648,#7649,#7650,#7651,#7652,
#7653,#7654,#7655,#7656,#7657,#7658,#7659,#7660,#7661,#7662,#7663,#7664,
#7665,#7666,#7667,#7668,#7669,#7670,#7671,#7672,#7673,#7674,#7675,#7676,
#7677),.UNSPECIFIED.,.F.,.F.,(4,3,3,3,3,3,3,3,3,3,3,3,3,3,3,3,3,3,3,3,3,
3,4),(-12.4772742666219,-12.386342772875,-12.3283412786589,-12.2415409750193,
-12.1547592718571,-12.0679755292032,-11.9811970627444,-11.8943972788186,
-11.8352076275126,-11.7482147332003,-11.6612380696607,-11.5742576640307,
-11.4872820225213,-11.4002860143297,-11.3420739763662,-11.2551423602584,
-11.1682278559083,-11.0813103241984,-10.9943978098696,-10.9074647519428,
-10.8489403252199,-10.7592881888023,-10.6751012271442),.UNSPECIFIED.);
#89=B_SPLINE_CURVE_WITH_KNOTS('',3,(#7707,#7708,#7709,#7710,#7711,#7712),
 .UNSPECIFIED.,.F.,.F.,(4,2,4),(-0.270403079816102,-0.13523083141612,-1.64625206816352E-5),
 .UNSPECIFIED.);
#90=B_SPLINE_CURVE_WITH_KNOTS('',3,(#7714,#7715,#7716,#7717,#7718,#7719),
 .UNSPECIFIED.,.F.,.F.,(4,2,4),(-0.292980681038648,-0.146437065077422,0.),
 .UNSPECIFIED.);
#91=B_SPLINE_CURVE_WITH_KNOTS('',3,(#7720,#7721,#7722,#7723,#7724,#7725,
#7726,#7727,#7728,#7729,#7730,#7731,#7732,#7733,#7734,#7735,#7736,#7737,
#7738,#7739,#7740,#7741,#7742,#7743,#7744,#7745,#7746,#7747,#7748,#7749,
#7750,#7751,#7752,#7753,#7754,#7755,#7756),.UNSPECIFIED.,.F.,.F.,(4,3,3,
3,3,3,3,3,3,3,3,3,4),(-15.2154843560458,-15.2119477690322,-15.1249068169761,
-15.034342832825,-14.947305252502,-14.8602673694158,-14.7732113197559,-14.7626508803718,
-14.6757146349977,-14.5887879934978,-14.5018740211044,-14.414949455508,
-14.3463120123156),.UNSPECIFIED.);
#92=B_SPLINE_CURVE_WITH_KNOTS('',3,(#7777,#7778,#7779,#7780,#7781,#7782),
 .UNSPECIFIED.,.F.,.F.,(4,2,4),(-0.125419138950074,-0.0626178594416655,
0.),.UNSPECIFIED.);
#93=B_SPLINE_CURVE_WITH_KNOTS('',3,(#7804,#7805,#7806,#7807,#7808,#7809),
 .UNSPECIFIED.,.F.,.F.,(4,2,4),(-0.11509764486976,-0.0575516446763736,0.),
 .UNSPECIFIED.);
#94=B_SPLINE_CURVE_WITH_KNOTS('',3,(#7811,#7812,#7813,#7814,#7815,#7816,
#7817,#7818,#7819,#7820,#7821,#7822,#7823,#7824,#7825,#7826,#7827,#7828,
#7829,#7830,#7831,#7832,#7833,#7834,#7835,#7836,#7837,#7838,#7839,#7840,
#7841,#7842,#7843,#7844,#7845,#7846,#7847,#7848,#7849,#7850,#7851,#7852,
#7853,#7854,#7855,#7856,#7857,#7858,#7859),.UNSPECIFIED.,.F.,.F.,(4,3,3,
3,3,3,3,3,3,3,3,3,3,3,3,3,4),(14.7080621488406,14.7945507604512,14.8810228978745,
14.9674879490283,15.0539552968216,15.1404593843328,15.2269782020299,15.3135524038241,
15.3746865735895,15.4609099016134,15.5470903095525,15.6332384449514,15.7193649306605,
15.8054913260564,15.8916146167529,15.9777597272694,16.0055641921085),
 .UNSPECIFIED.);
#95=B_SPLINE_CURVE_WITH_KNOTS('',3,(#7860,#7861,#7862,#7863,#7864,#7865),
 .UNSPECIFIED.,.F.,.F.,(4,2,4),(-0.115233993178556,-0.0536451184811805,
0.),.UNSPECIFIED.);
#96=B_SPLINE_CURVE_WITH_KNOTS('',3,(#7872,#7873,#7874,#7875,#7876,#7877,
#7878,#7879,#7880,#7881,#7882,#7883),.UNSPECIFIED.,.F.,.F.,(4,2,2,2,2,4),
(2.90713419165293,3.14556848854061,3.38400278542828,3.6300908538161,3.75313488801,
3.87617892220391),.UNSPECIFIED.);
#97=B_SPLINE_CURVE_WITH_KNOTS('',3,(#7885,#7886,#7887,#7888,#7889,#7890,
#7891,#7892,#7893,#7894,#7895,#7896),.UNSPECIFIED.,.F.,.F.,(4,2,2,2,2,4),
(0.,0.123044034193907,0.246088068387815,0.492176136775629,0.730610433663304,
0.969044730550978),.UNSPECIFIED.);
#98=B_SPLINE_CURVE_WITH_KNOTS('',3,(#7900,#7901,#7902,#7903,#7904,#7905,
#7906,#7907,#7908,#7909,#7910,#7911,#7912,#7913,#7914,#7915,#7916,#7917,
#7918,#7919,#7920,#7921),.UNSPECIFIED.,.F.,.F.,(4,2,2,2,2,2,2,2,2,2,4),
(0.969044730550978,1.20747902743865,1.44591332432633,1.69200139271414,1.81504542690805,
1.93808946110196,2.06113349529586,2.18417752948977,2.43026559787759,2.66869989476526,
2.90713419165293),.UNSPECIFIED.);
#99=B_SPLINE_CURVE_WITH_KNOTS('',3,(#7922,#7923,#7924,#7925,#7926,#7927),
 .UNSPECIFIED.,.F.,.F.,(4,2,4),(0.381327752557984,0.406901830999469,0.5388522709963),
 .UNSPECIFIED.);
#100=B_SPLINE_CURVE_WITH_KNOTS('',3,(#7928,#7929,#7930,#7931,#7932,#7933,
#7934,#7935),.UNSPECIFIED.,.F.,.F.,(4,2,2,4),(1.43219876356662,1.61728075708837,
1.82073167258811,1.87531375049552),.UNSPECIFIED.);
#101=B_SPLINE_CURVE_WITH_KNOTS('',3,(#7936,#7937,#7938,#7939),
 .UNSPECIFIED.,.F.,.F.,(4,4),(2.83774858360888,2.94879070536832),
 .UNSPECIFIED.);
#531=SHAPE_REPRESENTATION_RELATIONSHIP('SRR','None',#74564,#540);
#540=ADVANCED_BREP_SHAPE_REPRESENTATION('',(#558),#74520);
#549=STYLED_ITEM('',(#74612),#558);
#558=MANIFOLD_SOLID_BREP('Body1',#4728);
#602=FACE_BOUND('',#984,.T.);
#603=FACE_BOUND('',#989,.T.);
#604=FACE_BOUND('',#991,.T.);
#605=FACE_BOUND('',#994,.T.);
#606=FACE_BOUND('',#997,.T.);
#663=PLANE('',#5045);
#664=PLANE('',#5057);
#665=PLANE('',#5058);
#666=PLANE('',#5059);
#667=PLANE('',#5060);
#668=PLANE('',#5061);
#669=PLANE('',#5062);
#785=FACE_OUTER_BOUND('',#970,.T.);
#786=FACE_OUTER_BOUND('',#971,.T.);
#787=FACE_OUTER_BOUND('',#972,.T.);
#788=FACE_OUTER_BOUND('',#973,.T.);
#789=FACE_OUTER_BOUND('',#974,.T.);
#790=FACE_OUTER_BOUND('',#975,.T.);
#791=FACE_OUTER_BOUND('',#976,.T.);
#792=FACE_OUTER_BOUND('',#977,.T.);
#793=FACE_OUTER_BOUND('',#978,.T.);
#794=FACE_OUTER_BOUND('',#979,.T.);
#795=FACE_OUTER_BOUND('',#980,.T.);
#796=FACE_OUTER_BOUND('',#981,.T.);
#797=FACE_OUTER_BOUND('',#982,.T.);
#798=FACE_OUTER_BOUND('',#983,.T.);
#799=FACE_OUTER_BOUND('',#985,.T.);
#800=FACE_OUTER_BOUND('',#986,.T.);
#801=FACE_OUTER_BOUND('',#987,.T.);
#802=FACE_OUTER_BOUND('',#988,.T.);
#803=FACE_OUTER_BOUND('',#990,.T.);
#804=FACE_OUTER_BOUND('',#992,.T.);
#805=FACE_OUTER_BOUND('',#993,.T.);
#806=FACE_OUTER_BOUND('',#995,.T.);
#807=FACE_OUTER_BOUND('',#996,.T.);
#970=EDGE_LOOP('',(#3476,#3477,#3478,#3479));
#971=EDGE_LOOP('',(#3480,#3481,#3482,#3483,#3484));
#972=EDGE_LOOP('',(#3485,#3486,#3487,#3488));
#973=EDGE_LOOP('',(#3489,#3490,#3491,#3492));
#974=EDGE_LOOP('',(#3493,#3494,#3495,#3496,#3497));
#975=EDGE_LOOP('',(#3498,#3499,#3500));
#976=EDGE_LOOP('',(#3501,#3502,#3503,#3504,#3505,#3506,#3507,#3508,#3509,
#3510));
#977=EDGE_LOOP('',(#3511,#3512,#3513,#3514));
#978=EDGE_LOOP('',(#3515,#3516,#3517,#3518,#3519));
#979=EDGE_LOOP('',(#3520,#3521,#3522,#3523,#3524,#3525,#3526,#3527,#3528,
#3529));
#980=EDGE_LOOP('',(#3530,#3531,#3532,#3533));
#981=EDGE_LOOP('',(#3534,#3535,#3536));
#982=EDGE_LOOP('',(#3537,#3538,#3539,#3540));
#983=EDGE_LOOP('',(#3541,#3542,#3543,#3544,#3545,#3546,#3547,#3548,#3549));
#984=EDGE_LOOP('',(#3550,#3551,#3552,#3553,#3554,#3555,#3556,#3557,#3558,
#3559,#3560,#3561,#3562,#3563,#3564,#3565,#3566,#3567,#3568));
#985=EDGE_LOOP('',(#3569,#3570));
#986=EDGE_LOOP('',(#3571,#3572,#3573,#3574));
#987=EDGE_LOOP('',(#3575,#3576,#3577,#3578,#3579,#3580));
#988=EDGE_LOOP('',(#3581,#3582,#3583,#3584));
#989=EDGE_LOOP('',(#3585));
#990=EDGE_LOOP('',(#3586,#3587,#3588,#3589));
#991=EDGE_LOOP('',(#3590));
#992=EDGE_LOOP('',(#3591,#3592,#3593,#3594));
#993=EDGE_LOOP('',(#3595,#3596,#3597,#3598));
#994=EDGE_LOOP('',(#3599,#3600,#3601,#3602));
#995=EDGE_LOOP('',(#3603,#3604,#3605,#3606));
#996=EDGE_LOOP('',(#3607,#3608,#3609,#3610));
#997=EDGE_LOOP('',(#3611));
#1176=LINE('',#6460,#1373);
#1177=LINE('',#6484,#1374);
#1178=LINE('',#6558,#1375);
#1179=LINE('',#6853,#1376);
#1180=LINE('',#7870,#1377);
#1181=LINE('',#7898,#1378);
#1182=LINE('',#7944,#1379);
#1183=LINE('',#7949,#1380);
#1184=LINE('',#7951,#1381);
#1185=LINE('',#7953,#1382);
#1186=LINE('',#7954,#1383);
#1187=LINE('',#7957,#1384);
#1188=LINE('',#7959,#1385);
#1189=LINE('',#7960,#1386);
#1190=LINE('',#7963,#1387);
#1191=LINE('',#7964,#1388);
#1192=LINE('',#7967,#1389);
#1193=LINE('',#7968,#1390);
#1194=LINE('',#7970,#1391);
#1373=VECTOR('',#5672,6.11325);
#1374=VECTOR('',#5675,6.11325);
#1375=VECTOR('',#5680,5.13675);
#1376=VECTOR('',#5689,10.);
#1377=VECTOR('',#5702,7.5);
#1378=VECTOR('',#5703,7.5);
#1379=VECTOR('',#5712,6.);
#1380=VECTOR('',#5717,10.);
#1381=VECTOR('',#5718,10.);
#1382=VECTOR('',#5719,10.);
#1383=VECTOR('',#5720,10.);
#1384=VECTOR('',#5723,10.);
#1385=VECTOR('',#5724,10.);
#1386=VECTOR('',#5725,10.);
#1387=VECTOR('',#5728,10.);
#1388=VECTOR('',#5729,10.);
#1389=VECTOR('',#5732,10.);
#1390=VECTOR('',#5733,10.);
#1391=VECTOR('',#5736,10.);
#1508=CIRCLE('',#5040,6.11325);
#1509=CIRCLE('',#5042,5.13675);
#1510=CIRCLE('',#5046,6.11325);
#1511=CIRCLE('',#5051,7.5);
#1512=CIRCLE('',#5052,7.5);
#1513=CIRCLE('',#5056,6.);
#1695=VERTEX_POINT('',#6458);
#1696=VERTEX_POINT('',#6459);
#1697=VERTEX_POINT('',#6461);
#1698=VERTEX_POINT('',#6466);
#1699=VERTEX_POINT('',#6482);
#1700=VERTEX_POINT('',#6483);
#1701=VERTEX_POINT('',#6485);
#1702=VERTEX_POINT('',#6508);
#1703=VERTEX_POINT('',#6515);
#1704=VERTEX_POINT('',#6556);
#1705=VERTEX_POINT('',#6557);
#1706=VERTEX_POINT('',#6559);
#1707=VERTEX_POINT('',#6598);
#1708=VERTEX_POINT('',#6653);
#1709=VERTEX_POINT('',#6700);
#1710=VERTEX_POINT('',#6752);
#1711=VERTEX_POINT('',#6851);
#1712=VERTEX_POINT('',#6852);
#1713=VERTEX_POINT('',#6854);
#1714=VERTEX_POINT('',#7023);
#1715=VERTEX_POINT('',#7050);
#1716=VERTEX_POINT('',#7240);
#1717=VERTEX_POINT('',#7245);
#1718=VERTEX_POINT('',#7324);
#1719=VERTEX_POINT('',#7326);
#1720=VERTEX_POINT('',#7332);
#1721=VERTEX_POINT('',#7458);
#1722=VERTEX_POINT('',#7580);
#1723=VERTEX_POINT('',#7706);
#1724=VERTEX_POINT('',#7713);
#1725=VERTEX_POINT('',#7803);
#1726=VERTEX_POINT('',#7810);
#1727=VERTEX_POINT('',#7867);
#1728=VERTEX_POINT('',#7869);
#1729=VERTEX_POINT('',#7871);
#1730=VERTEX_POINT('',#7884);
#1731=VERTEX_POINT('',#7897);
#1732=VERTEX_POINT('',#7943);
#1733=VERTEX_POINT('',#7947);
#1734=VERTEX_POINT('',#7948);
#1735=VERTEX_POINT('',#7950);
#1736=VERTEX_POINT('',#7952);
#1737=VERTEX_POINT('',#7956);
#1738=VERTEX_POINT('',#7958);
#1739=VERTEX_POINT('',#7962);
#1740=VERTEX_POINT('',#7966);
#2439=EDGE_CURVE('',#1695,#1696,#1176,.T.);
#2440=EDGE_CURVE('',#1696,#1697,#60,.T.);
#2441=EDGE_CURVE('',#1698,#1697,#61,.T.);
#2442=EDGE_CURVE('',#1695,#1698,#62,.F.);
#2443=EDGE_CURVE('',#1699,#1700,#1177,.T.);
#2444=EDGE_CURVE('',#1701,#1699,#63,.F.);
#2445=EDGE_CURVE('',#1702,#1701,#64,.T.);
#2446=EDGE_CURVE('',#1703,#1702,#1508,.T.);
#2447=EDGE_CURVE('',#1703,#1700,#65,.T.);
#2448=EDGE_CURVE('',#1704,#1705,#1178,.T.);
#2449=EDGE_CURVE('',#1704,#1706,#66,.F.);
#2450=EDGE_CURVE('',#1707,#1706,#1509,.T.);
#2451=EDGE_CURVE('',#1707,#1705,#67,.T.);
#2452=EDGE_CURVE('',#1705,#1708,#68,.T.);
#2453=EDGE_CURVE('',#1709,#1708,#69,.T.);
#2454=EDGE_CURVE('',#1709,#1704,#70,.F.);
#2455=EDGE_CURVE('',#1700,#1710,#71,.T.);
#2456=EDGE_CURVE('',#1710,#1696,#72,.T.);
#2457=EDGE_CURVE('',#1699,#1695,#73,.F.);
#2458=EDGE_CURVE('',#1711,#1712,#1179,.T.);
#2459=EDGE_CURVE('',#1711,#1713,#1510,.T.);
#2460=EDGE_CURVE('',#1713,#1712,#74,.T.);
#2461=EDGE_CURVE('',#1714,#1698,#75,.T.);
#2462=EDGE_CURVE('',#1714,#1715,#76,.T.);
#2463=EDGE_CURVE('',#1708,#1715,#77,.T.);
#2464=EDGE_CURVE('',#1702,#1707,#78,.T.);
#2465=EDGE_CURVE('',#1715,#1716,#79,.T.);
#2466=EDGE_CURVE('',#1717,#1714,#80,.T.);
#2467=EDGE_CURVE('',#1717,#1716,#81,.T.);
#2468=EDGE_CURVE('',#1718,#1711,#47,.T.);
#2469=EDGE_CURVE('',#1719,#1718,#82,.T.);
#2470=EDGE_CURVE('',#1720,#1719,#83,.T.);
#2471=EDGE_CURVE('',#1720,#1713,#84,.T.);
#2472=EDGE_CURVE('',#1697,#1721,#85,.T.);
#2473=EDGE_CURVE('',#1706,#1703,#86,.T.);
#2474=EDGE_CURVE('',#1722,#1709,#87,.T.);
#2475=EDGE_CURVE('',#1721,#1722,#88,.T.);
#2476=EDGE_CURVE('',#1716,#1723,#89,.T.);
#2477=EDGE_CURVE('',#1724,#1717,#90,.T.);
#2478=EDGE_CURVE('',#1723,#1724,#91,.T.);
#2479=EDGE_CURVE('',#1712,#1720,#92,.T.);
#2480=EDGE_CURVE('',#1725,#1718,#93,.T.);
#2481=EDGE_CURVE('',#1726,#1725,#94,.T.);
#2482=EDGE_CURVE('',#1719,#1726,#95,.T.);
#2483=EDGE_CURVE('',#1727,#1727,#1511,.T.);
#2484=EDGE_CURVE('',#1727,#1728,#1180,.T.);
#2485=EDGE_CURVE('',#1728,#1729,#96,.T.);
#2486=EDGE_CURVE('',#1729,#1730,#97,.T.);
#2487=EDGE_CURVE('',#1730,#1731,#1181,.T.);
#2488=EDGE_CURVE('',#1731,#1731,#1512,.T.);
#2489=EDGE_CURVE('',#1730,#1728,#98,.T.);
#2490=EDGE_CURVE('',#1726,#1722,#99,.T.);
#2491=EDGE_CURVE('',#1723,#1724,#100,.T.);
#2492=EDGE_CURVE('',#1721,#1725,#101,.T.);
#2493=EDGE_CURVE('',#1728,#1732,#1182,.T.);
#2494=EDGE_CURVE('',#1732,#1732,#1513,.T.);
#2495=EDGE_CURVE('',#1733,#1734,#1183,.T.);
#2496=EDGE_CURVE('',#1734,#1735,#1184,.T.);
#2497=EDGE_CURVE('',#1735,#1736,#1185,.T.);
#2498=EDGE_CURVE('',#1736,#1733,#1186,.T.);
#2499=EDGE_CURVE('',#1737,#1734,#1187,.T.);
#2500=EDGE_CURVE('',#1738,#1737,#1188,.T.);
#2501=EDGE_CURVE('',#1735,#1738,#1189,.T.);
#2502=EDGE_CURVE('',#1739,#1738,#1190,.T.);
#2503=EDGE_CURVE('',#1736,#1739,#1191,.T.);
#2504=EDGE_CURVE('',#1740,#1739,#1192,.T.);
#2505=EDGE_CURVE('',#1733,#1740,#1193,.T.);
#2506=EDGE_CURVE('',#1737,#1740,#1194,.T.);
#3476=ORIENTED_EDGE('',*,*,#2439,.T.);
#3477=ORIENTED_EDGE('',*,*,#2440,.T.);
#3478=ORIENTED_EDGE('',*,*,#2441,.F.);
#3479=ORIENTED_EDGE('',*,*,#2442,.F.);
#3480=ORIENTED_EDGE('',*,*,#2443,.F.);
#3481=ORIENTED_EDGE('',*,*,#2444,.F.);
#3482=ORIENTED_EDGE('',*,*,#2445,.F.);
#3483=ORIENTED_EDGE('',*,*,#2446,.F.);
#3484=ORIENTED_EDGE('',*,*,#2447,.T.);
#3485=ORIENTED_EDGE('',*,*,#2448,.F.);
#3486=ORIENTED_EDGE('',*,*,#2449,.T.);
#3487=ORIENTED_EDGE('',*,*,#2450,.F.);
#3488=ORIENTED_EDGE('',*,*,#2451,.T.);
#3489=ORIENTED_EDGE('',*,*,#2448,.T.);
#3490=ORIENTED_EDGE('',*,*,#2452,.T.);
#3491=ORIENTED_EDGE('',*,*,#2453,.F.);
#3492=ORIENTED_EDGE('',*,*,#2454,.T.);
#3493=ORIENTED_EDGE('',*,*,#2443,.T.);
#3494=ORIENTED_EDGE('',*,*,#2455,.T.);
#3495=ORIENTED_EDGE('',*,*,#2456,.T.);
#3496=ORIENTED_EDGE('',*,*,#2439,.F.);
#3497=ORIENTED_EDGE('',*,*,#2457,.F.);
#3498=ORIENTED_EDGE('',*,*,#2458,.F.);
#3499=ORIENTED_EDGE('',*,*,#2459,.T.);
#3500=ORIENTED_EDGE('',*,*,#2460,.T.);
#3501=ORIENTED_EDGE('',*,*,#2461,.F.);
#3502=ORIENTED_EDGE('',*,*,#2462,.T.);
#3503=ORIENTED_EDGE('',*,*,#2463,.F.);
#3504=ORIENTED_EDGE('',*,*,#2452,.F.);
#3505=ORIENTED_EDGE('',*,*,#2451,.F.);
#3506=ORIENTED_EDGE('',*,*,#2464,.F.);
#3507=ORIENTED_EDGE('',*,*,#2445,.T.);
#3508=ORIENTED_EDGE('',*,*,#2444,.T.);
#3509=ORIENTED_EDGE('',*,*,#2457,.T.);
#3510=ORIENTED_EDGE('',*,*,#2442,.T.);
#3511=ORIENTED_EDGE('',*,*,#2465,.F.);
#3512=ORIENTED_EDGE('',*,*,#2462,.F.);
#3513=ORIENTED_EDGE('',*,*,#2466,.F.);
#3514=ORIENTED_EDGE('',*,*,#2467,.T.);
#3515=ORIENTED_EDGE('',*,*,#2468,.F.);
#3516=ORIENTED_EDGE('',*,*,#2469,.F.);
#3517=ORIENTED_EDGE('',*,*,#2470,.F.);
#3518=ORIENTED_EDGE('',*,*,#2471,.T.);
#3519=ORIENTED_EDGE('',*,*,#2459,.F.);
#3520=ORIENTED_EDGE('',*,*,#2472,.F.);
#3521=ORIENTED_EDGE('',*,*,#2440,.F.);
#3522=ORIENTED_EDGE('',*,*,#2456,.F.);
#3523=ORIENTED_EDGE('',*,*,#2455,.F.);
#3524=ORIENTED_EDGE('',*,*,#2447,.F.);
#3525=ORIENTED_EDGE('',*,*,#2473,.F.);
#3526=ORIENTED_EDGE('',*,*,#2449,.F.);
#3527=ORIENTED_EDGE('',*,*,#2454,.F.);
#3528=ORIENTED_EDGE('',*,*,#2474,.F.);
#3529=ORIENTED_EDGE('',*,*,#2475,.F.);
#3530=ORIENTED_EDGE('',*,*,#2476,.F.);
#3531=ORIENTED_EDGE('',*,*,#2467,.F.);
#3532=ORIENTED_EDGE('',*,*,#2477,.F.);
#3533=ORIENTED_EDGE('',*,*,#2478,.F.);
#3534=ORIENTED_EDGE('',*,*,#2479,.F.);
#3535=ORIENTED_EDGE('',*,*,#2460,.F.);
#3536=ORIENTED_EDGE('',*,*,#2471,.F.);
#3537=ORIENTED_EDGE('',*,*,#2480,.F.);
#3538=ORIENTED_EDGE('',*,*,#2481,.F.);
#3539=ORIENTED_EDGE('',*,*,#2482,.F.);
#3540=ORIENTED_EDGE('',*,*,#2469,.T.);
#3541=ORIENTED_EDGE('',*,*,#2483,.F.);
#3542=ORIENTED_EDGE('',*,*,#2484,.T.);
#3543=ORIENTED_EDGE('',*,*,#2485,.T.);
#3544=ORIENTED_EDGE('',*,*,#2486,.T.);
#3545=ORIENTED_EDGE('',*,*,#2487,.T.);
#3546=ORIENTED_EDGE('',*,*,#2488,.F.);
#3547=ORIENTED_EDGE('',*,*,#2487,.F.);
#3548=ORIENTED_EDGE('',*,*,#2489,.T.);
#3549=ORIENTED_EDGE('',*,*,#2484,.F.);
#3550=ORIENTED_EDGE('',*,*,#2480,.T.);
#3551=ORIENTED_EDGE('',*,*,#2468,.T.);
#3552=ORIENTED_EDGE('',*,*,#2458,.T.);
#3553=ORIENTED_EDGE('',*,*,#2479,.T.);
#3554=ORIENTED_EDGE('',*,*,#2470,.T.);
#3555=ORIENTED_EDGE('',*,*,#2482,.T.);
#3556=ORIENTED_EDGE('',*,*,#2490,.T.);
#3557=ORIENTED_EDGE('',*,*,#2474,.T.);
#3558=ORIENTED_EDGE('',*,*,#2453,.T.);
#3559=ORIENTED_EDGE('',*,*,#2463,.T.);
#3560=ORIENTED_EDGE('',*,*,#2465,.T.);
#3561=ORIENTED_EDGE('',*,*,#2476,.T.);
#3562=ORIENTED_EDGE('',*,*,#2491,.T.);
#3563=ORIENTED_EDGE('',*,*,#2477,.T.);
#3564=ORIENTED_EDGE('',*,*,#2466,.T.);
#3565=ORIENTED_EDGE('',*,*,#2461,.T.);
#3566=ORIENTED_EDGE('',*,*,#2441,.T.);
#3567=ORIENTED_EDGE('',*,*,#2472,.T.);
#3568=ORIENTED_EDGE('',*,*,#2492,.T.);
#3569=ORIENTED_EDGE('',*,*,#2478,.T.);
#3570=ORIENTED_EDGE('',*,*,#2491,.F.);
#3571=ORIENTED_EDGE('',*,*,#2481,.T.);
#3572=ORIENTED_EDGE('',*,*,#2492,.F.);
#3573=ORIENTED_EDGE('',*,*,#2475,.T.);
#3574=ORIENTED_EDGE('',*,*,#2490,.F.);
#3575=ORIENTED_EDGE('',*,*,#2486,.F.);
#3576=ORIENTED_EDGE('',*,*,#2485,.F.);
#3577=ORIENTED_EDGE('',*,*,#2493,.T.);
#3578=ORIENTED_EDGE('',*,*,#2494,.F.);
#3579=ORIENTED_EDGE('',*,*,#2493,.F.);
#3580=ORIENTED_EDGE('',*,*,#2489,.F.);
#3581=ORIENTED_EDGE('',*,*,#2495,.T.);
#3582=ORIENTED_EDGE('',*,*,#2496,.T.);
#3583=ORIENTED_EDGE('',*,*,#2497,.T.);
#3584=ORIENTED_EDGE('',*,*,#2498,.T.);
#3585=ORIENTED_EDGE('',*,*,#2483,.T.);
#3586=ORIENTED_EDGE('',*,*,#2499,.F.);
#3587=ORIENTED_EDGE('',*,*,#2500,.F.);
#3588=ORIENTED_EDGE('',*,*,#2501,.F.);
#3589=ORIENTED_EDGE('',*,*,#2496,.F.);
#3590=ORIENTED_EDGE('',*,*,#2494,.T.);
#3591=ORIENTED_EDGE('',*,*,#2501,.T.);
#3592=ORIENTED_EDGE('',*,*,#2502,.F.);
#3593=ORIENTED_EDGE('',*,*,#2503,.F.);
#3594=ORIENTED_EDGE('',*,*,#2497,.F.);
#3595=ORIENTED_EDGE('',*,*,#2503,.T.);
#3596=ORIENTED_EDGE('',*,*,#2504,.F.);
#3597=ORIENTED_EDGE('',*,*,#2505,.F.);
#3598=ORIENTED_EDGE('',*,*,#2498,.F.);
#3599=ORIENTED_EDGE('',*,*,#2464,.T.);
#3600=ORIENTED_EDGE('',*,*,#2450,.T.);
#3601=ORIENTED_EDGE('',*,*,#2473,.T.);
#3602=ORIENTED_EDGE('',*,*,#2446,.T.);
#3603=ORIENTED_EDGE('',*,*,#2505,.T.);
#3604=ORIENTED_EDGE('',*,*,#2506,.F.);
#3605=ORIENTED_EDGE('',*,*,#2499,.T.);
#3606=ORIENTED_EDGE('',*,*,#2495,.F.);
#3607=ORIENTED_EDGE('',*,*,#2506,.T.);
#3608=ORIENTED_EDGE('',*,*,#2504,.T.);
#3609=ORIENTED_EDGE('',*,*,#2502,.T.);
#3610=ORIENTED_EDGE('',*,*,#2500,.T.);
#3611=ORIENTED_EDGE('',*,*,#2488,.T.);
#4563=CYLINDRICAL_SURFACE('',#5038,6.11325);
#4564=CYLINDRICAL_SURFACE('',#5039,6.11325);
#4565=CYLINDRICAL_SURFACE('',#5041,5.13675);
#4566=CYLINDRICAL_SURFACE('',#5043,5.13675);
#4567=CYLINDRICAL_SURFACE('',#5044,6.11325);
#4568=CYLINDRICAL_SURFACE('',#5047,6.11325);
#4569=CYLINDRICAL_SURFACE('',#5048,6.11325);
#4570=CYLINDRICAL_SURFACE('',#5050,7.5);
#4571=CYLINDRICAL_SURFACE('',#5053,5.13675);
#4572=CYLINDRICAL_SURFACE('',#5054,5.13675);
#4573=CYLINDRICAL_SURFACE('',#5055,6.);
#4681=ADVANCED_FACE('',(#785),#4563,.F.);
#4682=ADVANCED_FACE('',(#786),#4564,.F.);
#4683=ADVANCED_FACE('',(#787),#4565,.F.);
#4684=ADVANCED_FACE('',(#788),#4566,.F.);
#4685=ADVANCED_FACE('',(#789),#4567,.F.);
#4686=ADVANCED_FACE('',(#790),#663,.T.);
#4687=ADVANCED_FACE('',(#791),#48,.F.);
#4688=ADVANCED_FACE('',(#792),#4568,.F.);
#4689=ADVANCED_FACE('',(#793),#4569,.F.);
#4690=ADVANCED_FACE('',(#794),#49,.F.);
#4691=ADVANCED_FACE('',(#795),#50,.F.);
#4692=ADVANCED_FACE('',(#796),#51,.F.);
#4693=ADVANCED_FACE('',(#797),#52,.F.);
#4694=ADVANCED_FACE('',(#798,#602),#4570,.F.);
#4695=ADVANCED_FACE('',(#799),#4571,.F.);
#4696=ADVANCED_FACE('',(#800),#4572,.F.);
#4697=ADVANCED_FACE('',(#801),#4573,.F.);
#4698=ADVANCED_FACE('',(#802,#603),#664,.F.);
#4699=ADVANCED_FACE('',(#803,#604),#665,.T.);
#4700=ADVANCED_FACE('',(#804),#666,.T.);
#4701=ADVANCED_FACE('',(#805,#605),#667,.T.);
#4702=ADVANCED_FACE('',(#806),#668,.T.);
#4703=ADVANCED_FACE('',(#807,#606),#669,.T.);
#4728=CLOSED_SHELL('',(#4681,#4682,#4683,#4684,#4685,#4686,#4687,#4688,
#4689,#4690,#4691,#4692,#4693,#4694,#4695,#4696,#4697,#4698,#4699,#4700,
#4701,#4702,#4703));
#5037=AXIS2_PLACEMENT_3D('',#6456,#5668,#5669);
#5038=AXIS2_PLACEMENT_3D('',#6457,#5670,#5671);
#5039=AXIS2_PLACEMENT_3D('',#6481,#5673,#5674);
#5040=AXIS2_PLACEMENT_3D('',#6516,#5676,#5677);
#5041=AXIS2_PLACEMENT_3D('',#6555,#5678,#5679);
#5042=AXIS2_PLACEMENT_3D('',#6599,#5681,#5682);
#5043=AXIS2_PLACEMENT_3D('',#6652,#5683,#5684);
#5044=AXIS2_PLACEMENT_3D('',#6751,#5685,#5686);
#5045=AXIS2_PLACEMENT_3D('',#6850,#5687,#5688);
#5046=AXIS2_PLACEMENT_3D('',#6855,#5690,#5691);
#5047=AXIS2_PLACEMENT_3D('',#7239,#5692,#5693);
#5048=AXIS2_PLACEMENT_3D('',#7323,#5694,#5695);
#5049=AXIS2_PLACEMENT_3D('',#7325,#5696,#5697);
#5050=AXIS2_PLACEMENT_3D('',#7866,#5698,#5699);
#5051=AXIS2_PLACEMENT_3D('',#7868,#5700,#5701);
#5052=AXIS2_PLACEMENT_3D('',#7899,#5704,#5705);
#5053=AXIS2_PLACEMENT_3D('',#7940,#5706,#5707);
#5054=AXIS2_PLACEMENT_3D('',#7941,#5708,#5709);
#5055=AXIS2_PLACEMENT_3D('',#7942,#5710,#5711);
#5056=AXIS2_PLACEMENT_3D('',#7945,#5713,#5714);
#5057=AXIS2_PLACEMENT_3D('',#7946,#5715,#5716);
#5058=AXIS2_PLACEMENT_3D('',#7955,#5721,#5722);
#5059=AXIS2_PLACEMENT_3D('',#7961,#5726,#5727);
#5060=AXIS2_PLACEMENT_3D('',#7965,#5730,#5731);
#5061=AXIS2_PLACEMENT_3D('',#7969,#5734,#5735);
#5062=AXIS2_PLACEMENT_3D('',#7971,#5737,#5738);
#5668=DIRECTION('axis',(0.,0.,1.));
#5669=DIRECTION('refdir',(1.,0.,0.));
#5670=DIRECTION('center_axis',(-1.,0.,0.));
#5671=DIRECTION('ref_axis',(0.,-0.609000462850127,-0.793169865948229));
#5672=DIRECTION('',(-1.,0.,0.));
#5673=DIRECTION('center_axis',(-1.,0.,0.));
#5674=DIRECTION('ref_axis',(0.,-0.609000462850127,-0.793169865948229));
#5675=DIRECTION('',(-1.,0.,0.));
#5676=DIRECTION('center_axis',(-1.,0.,0.));
#5677=DIRECTION('ref_axis',(0.,1.,0.));
#5678=DIRECTION('center_axis',(-1.,0.,0.));
#5679=DIRECTION('ref_axis',(0.,0.859771171146174,-0.51067948193161));
#5680=DIRECTION('',(-1.,0.,0.));
#5681=DIRECTION('center_axis',(-1.,0.,0.));
#5682=DIRECTION('ref_axis',(0.,1.,0.));
#5683=DIRECTION('center_axis',(-1.,0.,0.));
#5684=DIRECTION('ref_axis',(0.,0.936836199765117,-0.3497684016741));
#5685=DIRECTION('center_axis',(-1.,0.,0.));
#5686=DIRECTION('ref_axis',(0.,-0.609000462850127,-0.793169865948229));
#5687=DIRECTION('center_axis',(1.,0.,0.));
#5688=DIRECTION('ref_axis',(0.,0.,-1.));
#5689=DIRECTION('',(0.,-1.,0.));
#5690=DIRECTION('center_axis',(1.,0.,0.));
#5691=DIRECTION('ref_axis',(0.,1.,0.));
#5692=DIRECTION('center_axis',(-1.,0.,0.));
#5693=DIRECTION('ref_axis',(0.,1.,0.));
#5694=DIRECTION('center_axis',(-1.,0.,0.));
#5695=DIRECTION('ref_axis',(0.,1.,0.));
#5696=DIRECTION('center_axis',(0.882978451059903,-0.305829609536471,0.356114173959174));
#5697=DIRECTION('ref_axis',(0.46437508102478,0.679952147198259,-0.5674688199749));
#5698=DIRECTION('center_axis',(0.,1.,0.));
#5699=DIRECTION('ref_axis',(1.,0.,0.));
#5700=DIRECTION('center_axis',(0.,1.,0.));
#5701=DIRECTION('ref_axis',(1.,0.,0.));
#5702=DIRECTION('',(0.,1.,0.));
#5703=DIRECTION('',(0.,1.,0.));
#5704=DIRECTION('center_axis',(0.,-1.,0.));
#5705=DIRECTION('ref_axis',(1.,0.,0.));
#5706=DIRECTION('center_axis',(-1.,0.,0.));
#5707=DIRECTION('ref_axis',(0.,1.,0.));
#5708=DIRECTION('center_axis',(-1.,0.,0.));
#5709=DIRECTION('ref_axis',(0.,1.,0.));
#5710=DIRECTION('center_axis',(-1.,0.,0.));
#5711=DIRECTION('ref_axis',(0.,1.,0.));
#5712=DIRECTION('',(-1.,0.,0.));
#5713=DIRECTION('center_axis',(1.,0.,0.));
#5714=DIRECTION('ref_axis',(0.,1.,0.));
#5715=DIRECTION('center_axis',(0.,1.,0.));
#5716=DIRECTION('ref_axis',(1.,0.,0.));
#5717=DIRECTION('',(-1.,0.,0.));
#5718=DIRECTION('',(0.,0.,-1.));
#5719=DIRECTION('',(1.,0.,0.));
#5720=DIRECTION('',(0.,0.,1.));
#5721=DIRECTION('center_axis',(-1.,0.,0.));
#5722=DIRECTION('ref_axis',(0.,0.,1.));
#5723=DIRECTION('',(0.,-1.,0.));
#5724=DIRECTION('',(0.,0.,1.));
#5725=DIRECTION('',(0.,1.,0.));
#5726=DIRECTION('center_axis',(0.,0.,-1.));
#5727=DIRECTION('ref_axis',(-1.,0.,0.));
#5728=DIRECTION('',(-1.,0.,0.));
#5729=DIRECTION('',(0.,1.,0.));
#5730=DIRECTION('center_axis',(1.,0.,0.));
#5731=DIRECTION('ref_axis',(0.,0.,-1.));
#5732=DIRECTION('',(0.,0.,-1.));
#5733=DIRECTION('',(0.,1.,0.));
#5734=DIRECTION('center_axis',(0.,0.,1.));
#5735=DIRECTION('ref_axis',(1.,0.,0.));
#5736=DIRECTION('',(1.,0.,0.));
#5737=DIRECTION('center_axis',(0.,1.,0.));
#5738=DIRECTION('ref_axis',(1.,0.,0.));
#6456=CARTESIAN_POINT('',(0.,0.,0.));
#6457=CARTESIAN_POINT('Origin',(189.09641784506,0.,335.));
#6458=CARTESIAN_POINT('',(182.497067674234,3.72297189708675,339.84884582308));
#6459=CARTESIAN_POINT('',(182.351531742639,3.7230579181248,339.848957366357));
#6460=CARTESIAN_POINT('',(189.09641784506,3.72297207951854,339.848845683008));
#6461=CARTESIAN_POINT('',(182.22440740295,5.47906074734768,337.711405334762));
#6462=CARTESIAN_POINT('Ctrl Pts',(182.351531742639,3.72305791812513,339.848957366357));
#6463=CARTESIAN_POINT('Ctrl Pts',(182.309156962742,4.46015191372697,339.282216531334));
#6464=CARTESIAN_POINT('Ctrl Pts',(182.266782182846,5.0665419705826,338.545000890668));
#6465=CARTESIAN_POINT('Ctrl Pts',(182.22440740295,5.47906074734771,337.711405334762));
#6466=CARTESIAN_POINT('',(182.352165757496,5.64138616135816,337.35555453857));
#6467=CARTESIAN_POINT('Ctrl Pts',(182.352160408299,5.64119776293606,337.355570708331));
#6468=CARTESIAN_POINT('Ctrl Pts',(182.347280418627,5.63503809829326,337.370322074647));
#6469=CARTESIAN_POINT('Ctrl Pts',(182.342360083051,5.62882375230088,337.385041670668));
#6470=CARTESIAN_POINT('Ctrl Pts',(182.301724441946,5.57746887366511,337.505365888699));
#6471=CARTESIAN_POINT('Ctrl Pts',(182.263984346319,5.52957139421465,337.609336160882));
#6472=CARTESIAN_POINT('Ctrl Pts',(182.22440740295,5.47906074734761,337.711405334762));
#6473=CARTESIAN_POINT('Ctrl Pts',(182.352270629205,5.64116224684411,337.355655761626));
#6474=CARTESIAN_POINT('Ctrl Pts',(182.367004937392,5.5152148489162,337.65726591955));
#6475=CARTESIAN_POINT('Ctrl Pts',(182.38167825968,5.36528272706277,337.94828699133));
#6476=CARTESIAN_POINT('Ctrl Pts',(182.411323504127,5.02168948100245,338.501373249097));
#6477=CARTESIAN_POINT('Ctrl Pts',(182.426246036053,4.82892822965015,338.762768314849));
#6478=CARTESIAN_POINT('Ctrl Pts',(182.460098215889,4.3471640672988,339.317707503377));
#6479=CARTESIAN_POINT('Ctrl Pts',(182.47861721716,4.04778944020427,339.599449032827));
#6480=CARTESIAN_POINT('Ctrl Pts',(182.497067674234,3.72297189708706,339.84884582308));
#6481=CARTESIAN_POINT('Origin',(189.09641784506,0.,335.));
#6482=CARTESIAN_POINT('',(184.246855413009,3.72297205899879,339.848845698763));
#6483=CARTESIAN_POINT('',(184.10166737808,3.72297207951882,339.848845683008));
#6484=CARTESIAN_POINT('',(189.09641784506,3.72297207951854,339.848845683008));
#6485=CARTESIAN_POINT('',(184.866944866212,-6.11325015325735,335.00025044505));
#6486=CARTESIAN_POINT('Ctrl Pts',(184.246855413009,3.72297205899967,339.848845698763));
#6487=CARTESIAN_POINT('Ctrl Pts',(184.268934436031,3.33920697021122,340.143502776249));
#6488=CARTESIAN_POINT('Ctrl Pts',(184.291464041663,2.92094987252177,340.392223513158));
#6489=CARTESIAN_POINT('Ctrl Pts',(184.340221220368,1.93946808592249,340.827132353816));
#6490=CARTESIAN_POINT('Ctrl Pts',(184.366324208566,1.37080299567188,340.986478115408));
#6491=CARTESIAN_POINT('Ctrl Pts',(184.411226219626,0.40085064572472,341.112585291422));
#6492=CARTESIAN_POINT('Ctrl Pts',(184.429328483896,0.0095859947715813,341.125708129067));
#6493=CARTESIAN_POINT('Ctrl Pts',(184.476014395384,-1.0175552976218,341.061694134485));
#6494=CARTESIAN_POINT('Ctrl Pts',(184.504435437676,-1.64471261302678,340.922371502746));
#6495=CARTESIAN_POINT('Ctrl Pts',(184.551841454068,-2.60324007796866,340.545113175205));
#6496=CARTESIAN_POINT('Ctrl Pts',(184.569886367204,-2.95298225246032,340.367034005226));
#6497=CARTESIAN_POINT('Ctrl Pts',(184.605223128158,-3.61305626692964,339.94676455908));
#6498=CARTESIAN_POINT('Ctrl Pts',(184.622723901052,-3.92191967308958,339.705656125618));
#6499=CARTESIAN_POINT('Ctrl Pts',(184.658511598607,-4.49155593275061,339.165687607535));
#6500=CARTESIAN_POINT('Ctrl Pts',(184.676723696593,-4.75060287248685,338.867659608251));
#6501=CARTESIAN_POINT('Ctrl Pts',(184.723589464835,-5.34323436716115,338.035695073479));
#6502=CARTESIAN_POINT('Ctrl Pts',(184.751252957232,-5.62644634462081,337.471579081712));
#6503=CARTESIAN_POINT('Ctrl Pts',(184.794456244581,-5.91605090024649,336.572482643603));
#6504=CARTESIAN_POINT('Ctrl Pts',(184.809100767287,-5.98963528962925,336.263576346589));
#6505=CARTESIAN_POINT('Ctrl Pts',(184.83828269457,-6.08838679889893,335.636077797764));
#6506=CARTESIAN_POINT('Ctrl Pts',(184.852615078266,-6.11323696023334,335.318411729172));
#6507=CARTESIAN_POINT('Ctrl Pts',(184.866945140388,-6.11324999486967,335.000250451567));
#6508=CARTESIAN_POINT('',(185.231676812499,-1.57888188187692,329.094159029776));
#6509=CARTESIAN_POINT('Ctrl Pts',(185.231676812499,-1.57888188187676,329.094159029776));
#6510=CARTESIAN_POINT('Ctrl Pts',(185.187737705833,-2.51057908317658,329.343241224495));
#6511=CARTESIAN_POINT('Ctrl Pts',(185.099859492502,-4.2531939892229,330.290287295343));
#6512=CARTESIAN_POINT('Ctrl Pts',(184.978279148315,-5.80226434466389,332.555945898845));
#6513=CARTESIAN_POINT('Ctrl Pts',(184.900637910794,-6.11262810662625,334.260548714089));
#6514=CARTESIAN_POINT('Ctrl Pts',(184.866935779939,-6.11326624072883,335.000250028895));
#6515=CARTESIAN_POINT('',(185.231464663099,1.57895204657858,329.094077731008));
#6516=CARTESIAN_POINT('Origin',(185.231676812499,0.,335.));
#6517=CARTESIAN_POINT('Ctrl Pts',(185.231408519459,1.57891980348589,329.094169167961));
#6518=CARTESIAN_POINT('Ctrl Pts',(185.210757145151,1.13681385221908,328.975972446527));
#6519=CARTESIAN_POINT('Ctrl Pts',(185.190336444102,0.68283589441395,328.907792814077));
#6520=CARTESIAN_POINT('Ctrl Pts',(185.149007405165,-0.22033833777906,328.874452483892));
#6521=CARTESIAN_POINT('Ctrl Pts',(185.128252990665,-0.666646880717682,328.906851779263));
#6522=CARTESIAN_POINT('Ctrl Pts',(185.094374985324,-1.39805812041619,329.041327412546));
#6523=CARTESIAN_POINT('Ctrl Pts',(185.081079478582,-1.68636324840246,329.116418570456));
#6524=CARTESIAN_POINT('Ctrl Pts',(185.032407357034,-2.70956750800716,329.464344394618));
#6525=CARTESIAN_POINT('Ctrl Pts',(184.996011299734,-3.39575068278064,329.856645196845));
#6526=CARTESIAN_POINT('Ctrl Pts',(184.942820817711,-4.28726067841481,330.624393229993));
#6527=CARTESIAN_POINT('Ctrl Pts',(184.925290369686,-4.55984109234911,330.909231098686));
#6528=CARTESIAN_POINT('Ctrl Pts',(184.883954763866,-5.12252800957322,331.623899404652));
#6529=CARTESIAN_POINT('Ctrl Pts',(184.859969757072,-5.38921493978292,332.068330999931));
#6530=CARTESIAN_POINT('Ctrl Pts',(184.818554092538,-5.75387511572488,332.89831036936));
#6531=CARTESIAN_POINT('Ctrl Pts',(184.801200855331,-5.87629802858345,333.269882635371));
#6532=CARTESIAN_POINT('Ctrl Pts',(184.756766777966,-6.09343376380386,334.229308936403));
#6533=CARTESIAN_POINT('Ctrl Pts',(184.729309773233,-6.13945282222875,334.824024973921));
#6534=CARTESIAN_POINT('Ctrl Pts',(184.684270483466,-6.07253416191094,335.805219443325));
#6535=CARTESIAN_POINT('Ctrl Pts',(184.666907708606,-6.0087844673568,336.191034156922));
#6536=CARTESIAN_POINT('Ctrl Pts',(184.621708365516,-5.75182080730419,337.159263264515));
#6537=CARTESIAN_POINT('Ctrl Pts',(184.593444189998,-5.50711706799555,337.723502312827));
#6538=CARTESIAN_POINT('Ctrl Pts',(184.547548627562,-4.97589630068615,338.572745620514));
#6539=CARTESIAN_POINT('Ctrl Pts',(184.53018003246,-4.73779610431471,338.882955921816));
#6540=CARTESIAN_POINT('Ctrl Pts',(184.476580942928,-3.92765088339003,339.752067851529));
#6541=CARTESIAN_POINT('Ctrl Pts',(184.439464154545,-3.27449478949327,340.22362693388));
#6542=CARTESIAN_POINT('Ctrl Pts',(184.385690918484,-2.1896798842563,340.721328010574));
#6543=CARTESIAN_POINT('Ctrl Pts',(184.367997331634,-1.8149967898242,340.850989257694));
#6544=CARTESIAN_POINT('Ctrl Pts',(184.332218877124,-1.05262541283211,341.034467978713));
#6545=CARTESIAN_POINT('Ctrl Pts',(184.314227942815,-0.667020259991067,341.089162340613));
#6546=CARTESIAN_POINT('Ctrl Pts',(184.278398981821,0.111536129765465,341.124712743585));
#6547=CARTESIAN_POINT('Ctrl Pts',(184.260932970875,0.502727641306943,341.105064727192));
#6548=CARTESIAN_POINT('Ctrl Pts',(184.214136410801,1.53067764544669,340.953907940929));
#6549=CARTESIAN_POINT('Ctrl Pts',(184.1842683051,2.15291708630206,340.758200620928));
#6550=CARTESIAN_POINT('Ctrl Pts',(184.136654629982,3.0817633410511,340.2940369392));
#6551=CARTESIAN_POINT('Ctrl Pts',(184.119272559744,3.41331187873858,340.086589962314));
#6552=CARTESIAN_POINT('Ctrl Pts',(184.101672843366,3.72287595009632,339.848919490427));
#6553=CARTESIAN_POINT('Ctrl Pts',(184.101670110764,3.72292401514821,339.848882587113));
#6554=CARTESIAN_POINT('Ctrl Pts',(184.101667378079,3.72297207952784,339.848845683001));
#6555=CARTESIAN_POINT('Origin',(185.231676812499,0.,335.));
#6556=CARTESIAN_POINT('',(184.058316793539,-4.81229327647336,336.796673031942));
#6557=CARTESIAN_POINT('',(183.581261447482,-4.81229344167014,336.796672589472));
#6558=CARTESIAN_POINT('',(185.231676812499,-4.81229334914346,336.796672837299));
#6559=CARTESIAN_POINT('',(185.231676812499,3.87994761181556,338.366334370211));
#6560=CARTESIAN_POINT('Ctrl Pts',(185.231676812499,3.87994761181582,338.366334370211));
#6561=CARTESIAN_POINT('Ctrl Pts',(185.20996580513,4.14235680482802,338.063888501864));
#6562=CARTESIAN_POINT('Ctrl Pts',(185.188753847695,4.36850674913513,337.731793007431));
#6563=CARTESIAN_POINT('Ctrl Pts',(185.145841871396,4.73497299547714,337.029670755389));
#6564=CARTESIAN_POINT('Ctrl Pts',(185.124297691399,4.87586902127356,336.662954808833));
#6565=CARTESIAN_POINT('Ctrl Pts',(185.088641172671,5.03911669330309,336.030508488665));
#6566=CARTESIAN_POINT('Ctrl Pts',(185.074632630748,5.08505461986033,335.772571767282));
#6567=CARTESIAN_POINT('Ctrl Pts',(185.024001495001,5.17911272059516,334.834079504077));
#6568=CARTESIAN_POINT('Ctrl Pts',(184.986563269637,5.1114288291029,334.149117473459));
#6569=CARTESIAN_POINT('Ctrl Pts',(184.931866564113,4.81520318126492,333.180754559098));
#6570=CARTESIAN_POINT('Ctrl Pts',(184.91425665323,4.6879575595803,332.874231121232));
#6571=CARTESIAN_POINT('Ctrl Pts',(184.878406205672,4.37574190234418,332.289018376107));
#6572=CARTESIAN_POINT('Ctrl Pts',(184.860242387235,4.19133006282589,332.011810013501));
#6573=CARTESIAN_POINT('Ctrl Pts',(184.823844294599,3.77165501678537,331.49699049157));
#6574=CARTESIAN_POINT('Ctrl Pts',(184.805957392279,3.53738598463557,331.260565721072));
#6575=CARTESIAN_POINT('Ctrl Pts',(184.75156741732,2.75745710874045,330.612808226125));
#6576=CARTESIAN_POINT('Ctrl Pts',(184.714210704466,2.15146534302681,330.285960234983));
#6577=CARTESIAN_POINT('Ctrl Pts',(184.659475360251,1.18310823591439,329.990426889));
#6578=CARTESIAN_POINT('Ctrl Pts',(184.641904078175,0.85821770171409,329.924663998108));
#6579=CARTESIAN_POINT('Ctrl Pts',(184.606089385025,0.198282503839793,329.856304065841));
#6580=CARTESIAN_POINT('Ctrl Pts',(184.587920312546,-0.13523862490782,329.854261738142));
#6581=CARTESIAN_POINT('Ctrl Pts',(184.533279894219,-1.12812501165542,329.944824830453));
#6582=CARTESIAN_POINT('Ctrl Pts',(184.498451887637,-1.7717130728769,330.132915585397));
#6583=CARTESIAN_POINT('Ctrl Pts',(184.443749858932,-2.66284907206899,330.594266702118));
#6584=CARTESIAN_POINT('Ctrl Pts',(184.425051832764,-2.94787866512476,330.779660956538));
#6585=CARTESIAN_POINT('Ctrl Pts',(184.388767227444,-3.47015821111336,331.198264076558));
#6586=CARTESIAN_POINT('Ctrl Pts',(184.371238350057,-3.70726722602787,331.429093672636));
#6587=CARTESIAN_POINT('Ctrl Pts',(184.335462940532,-4.13614372007297,331.935718384815));
#6588=CARTESIAN_POINT('Ctrl Pts',(184.317287363418,-4.32637787769082,332.210744097465));
#6589=CARTESIAN_POINT('Ctrl Pts',(184.262735370472,-4.8103228805498,333.080422073587));
#6590=CARTESIAN_POINT('Ctrl Pts',(184.22796605832,-5.01733792261535,333.715348928986));
#6591=CARTESIAN_POINT('Ctrl Pts',(184.174569905377,-5.13728177955315,334.689163986469));
#6592=CARTESIAN_POINT('Ctrl Pts',(184.1569893391,-5.14666817789588,335.009218592103));
#6593=CARTESIAN_POINT('Ctrl Pts',(184.121609678241,-5.10520666186254,335.657091153077));
#6594=CARTESIAN_POINT('Ctrl Pts',(184.104081307411,-5.05252221416993,335.983324333829));
#6595=CARTESIAN_POINT('Ctrl Pts',(184.077035990567,-4.92499983736479,336.469901749377));
#6596=CARTESIAN_POINT('Ctrl Pts',(184.067700098037,-4.8726894053407,336.634905209024));
#6597=CARTESIAN_POINT('Ctrl Pts',(184.058316793539,-4.81229327647345,336.796673031942));
#6598=CARTESIAN_POINT('',(185.231660786429,-3.87998480257461,338.366291504652));
#6599=CARTESIAN_POINT('Origin',(185.231676812499,0.,335.));
#6600=CARTESIAN_POINT('Ctrl Pts',(185.231660786429,-3.87998480257461,338.366291504652));
#6601=CARTESIAN_POINT('Ctrl Pts',(185.198841754409,-3.48679804038719,338.819478241377));
#6602=CARTESIAN_POINT('Ctrl Pts',(185.16716547498,-3.01724325598196,339.200286613357));
#6603=CARTESIAN_POINT('Ctrl Pts',(185.12378319743,-2.31888914664931,339.587858377999));
#6604=CARTESIAN_POINT('Ctrl Pts',(185.112888660786,-2.13968347867559,339.674125022322));
#6605=CARTESIAN_POINT('Ctrl Pts',(185.065810758349,-1.34414494710687,340.001722621249));
#6606=CARTESIAN_POINT('Ctrl Pts',(185.031025840614,-0.689409600570319,340.133095870716));
#6607=CARTESIAN_POINT('Ctrl Pts',(184.985849981913,0.138732706103458,340.137575612723));
#6608=CARTESIAN_POINT('Ctrl Pts',(184.976722348467,0.305196459457193,340.130378620157));
#6609=CARTESIAN_POINT('Ctrl Pts',(184.93117040401,1.13444531613264,340.054018755214));
#6610=CARTESIAN_POINT('Ctrl Pts',(184.896179138579,1.77969160026001,339.864439680823));
#6611=CARTESIAN_POINT('Ctrl Pts',(184.841625647083,2.6657547103338,339.403470072734));
#6612=CARTESIAN_POINT('Ctrl Pts',(184.823400079311,2.9451848259215,339.221693010019));
#6613=CARTESIAN_POINT('Ctrl Pts',(184.787552880288,3.46219644347254,338.808891037211));
#6614=CARTESIAN_POINT('Ctrl Pts',(184.770004716252,3.69899443635314,338.579370792128));
#6615=CARTESIAN_POINT('Ctrl Pts',(184.734481342641,4.12615259863405,338.07734591993));
#6616=CARTESIAN_POINT('Ctrl Pts',(184.716368530761,4.31535007448866,337.805874728676));
#6617=CARTESIAN_POINT('Ctrl Pts',(184.669070759649,4.73972687988867,337.0513458403));
#6618=CARTESIAN_POINT('Ctrl Pts',(184.64070517982,4.92765582124248,336.546358950252));
#6619=CARTESIAN_POINT('Ctrl Pts',(184.593828157937,5.09981772532086,335.697912186798));
#6620=CARTESIAN_POINT('Ctrl Pts',(184.575660754802,5.1341253925422,335.368748612603));
#6621=CARTESIAN_POINT('Ctrl Pts',(184.539500817174,5.13910858994622,334.705249812477));
#6622=CARTESIAN_POINT('Ctrl Pts',(184.521602036035,5.10916052483512,334.372464308965));
#6623=CARTESIAN_POINT('Ctrl Pts',(184.467945480004,4.92340967754059,333.390844320072));
#6624=CARTESIAN_POINT('Ctrl Pts',(184.431436715369,4.67366577046203,332.767022387495));
#6625=CARTESIAN_POINT('Ctrl Pts',(184.377255848456,4.12740600091846,331.923326514062));
#6626=CARTESIAN_POINT('Ctrl Pts',(184.359207055715,3.91516063337641,331.657409171325));
#6627=CARTESIAN_POINT('Ctrl Pts',(184.331665015962,3.56184547559044,331.294967774504));
#6628=CARTESIAN_POINT('Ctrl Pts',(184.322529305878,3.43970202932531,331.181301770471));
#6629=CARTESIAN_POINT('Ctrl Pts',(184.27753117341,2.81129293142445,330.651161764138));
#6630=CARTESIAN_POINT('Ctrl Pts',(184.243018370146,2.23405572599016,330.328302552668));
#6631=CARTESIAN_POINT('Ctrl Pts',(184.198246245456,1.45348912444086,330.070360091181));
#6632=CARTESIAN_POINT('Ctrl Pts',(184.189113003422,1.29278305477879,330.025797386536));
#6633=CARTESIAN_POINT('Ctrl Pts',(184.143877899258,0.486418116876675,329.843922724558));
#6634=CARTESIAN_POINT('Ctrl Pts',(184.109167450003,-0.179347486611541,329.824135504527));
#6635=CARTESIAN_POINT('Ctrl Pts',(184.064102325035,-0.994987552158871,329.957783832522));
#6636=CARTESIAN_POINT('Ctrl Pts',(184.054973186473,-1.15795156059106,329.992696142295));
#6637=CARTESIAN_POINT('Ctrl Pts',(184.009497659063,-1.96135003293104,330.206135307985));
#6638=CARTESIAN_POINT('Ctrl Pts',(183.974577203188,-2.56457202387815,330.49988808083));
#6639=CARTESIAN_POINT('Ctrl Pts',(183.920143775137,-3.36032431538043,331.100655938906));
#6640=CARTESIAN_POINT('Ctrl Pts',(183.901920970343,-3.60552434750443,331.326191891106));
#6641=CARTESIAN_POINT('Ctrl Pts',(183.866047047229,-4.04693461136795,331.819270717901));
#6642=CARTESIAN_POINT('Ctrl Pts',(183.848470886864,-4.24253554603068,332.08527680355));
#6643=CARTESIAN_POINT('Ctrl Pts',(183.812937838096,-4.58051914075442,332.651785905477));
#6644=CARTESIAN_POINT('Ctrl Pts',(183.794832750312,-4.72197314197139,332.951044125878));
#6645=CARTESIAN_POINT('Ctrl Pts',(183.740138191902,-5.06063518098444,333.892815761633));
#6646=CARTESIAN_POINT('Ctrl Pts',(183.704937726923,-5.16180369180752,334.562203161041));
#6647=CARTESIAN_POINT('Ctrl Pts',(183.65014115901,-5.11653344930504,335.563074239064));
#6648=CARTESIAN_POINT('Ctrl Pts',(183.632024523124,-5.06957717985736,335.891832003873));
#6649=CARTESIAN_POINT('Ctrl Pts',(183.603097831844,-4.94319086685525,336.411558018397));
#6650=CARTESIAN_POINT('Ctrl Pts',(183.592181128069,-4.88340826534985,336.606195258429));
#6651=CARTESIAN_POINT('Ctrl Pts',(183.581261447482,-4.81229344167016,336.796672589472));
#6652=CARTESIAN_POINT('Origin',(185.231676812499,0.,335.));
#6653=CARTESIAN_POINT('',(182.104574390455,-4.16808369392632,331.997787668581));
#6654=CARTESIAN_POINT('Ctrl Pts',(183.581261447482,-4.81229344167014,336.796672589472));
#6655=CARTESIAN_POINT('Ctrl Pts',(183.574404858247,-4.76763965069489,336.916275430142));
#6656=CARTESIAN_POINT('Ctrl Pts',(183.567545028061,-4.71851788329508,337.03423801728));
#6657=CARTESIAN_POINT('Ctrl Pts',(183.525857405484,-4.39553174791915,337.734944741595));
#6658=CARTESIAN_POINT('Ctrl Pts',(183.490590408521,-4.01852059594133,338.263762155306));
#6659=CARTESIAN_POINT('Ctrl Pts',(183.447056524281,-3.43330383098911,338.824448809187));
#6660=CARTESIAN_POINT('Ctrl Pts',(183.438122189421,-3.30740520662722,338.93383446743));
#6661=CARTESIAN_POINT('Ctrl Pts',(183.393766963293,-2.66213201654426,339.441563714041));
#6662=CARTESIAN_POINT('Ctrl Pts',(183.35793605831,-2.07521296953646,339.744254881504));
#6663=CARTESIAN_POINT('Ctrl Pts',(183.313831604382,-1.28730799481885,339.975625212872));
#6664=CARTESIAN_POINT('Ctrl Pts',(183.304891260124,-1.12511665638188,340.014790067098));
#6665=CARTESIAN_POINT('Ctrl Pts',(183.277525250885,-0.627891302656741,340.109516229218));
#6666=CARTESIAN_POINT('Ctrl Pts',(183.258850647331,-0.289003227088744,340.139832050651));
#6667=CARTESIAN_POINT('Ctrl Pts',(183.204067553403,0.715942364873389,340.129974231577));
#6668=CARTESIAN_POINT('Ctrl Pts',(183.169051486757,1.37392207659993,339.994149660602));
#6669=CARTESIAN_POINT('Ctrl Pts',(183.095925320236,2.60572135352441,339.477242136658));
#6670=CARTESIAN_POINT('Ctrl Pts',(183.060540187497,3.16708981082988,339.099392149873));
#6671=CARTESIAN_POINT('Ctrl Pts',(182.993542234995,4.03667924256993,338.226056893305));
#6672=CARTESIAN_POINT('Ctrl Pts',(182.962816006145,4.36528727345767,337.765237843109));
#6673=CARTESIAN_POINT('Ctrl Pts',(182.914826762285,4.75825638268382,336.963323415389));
#6674=CARTESIAN_POINT('Ctrl Pts',(182.897101413311,4.8747897302867,336.652894821662));
#6675=CARTESIAN_POINT('Ctrl Pts',(182.860929234834,5.04653726178304,336.013952186779));
#6676=CARTESIAN_POINT('Ctrl Pts',(182.842826325575,5.10135136518025,335.686921483203));
#6677=CARTESIAN_POINT('Ctrl Pts',(182.806976985386,5.14737805903147,335.026063851458));
#6678=CARTESIAN_POINT('Ctrl Pts',(182.78931135407,5.13832742675459,334.693782453588));
#6679=CARTESIAN_POINT('Ctrl Pts',(182.735918922984,5.01599852377635,333.71227950727));
#6680=CARTESIAN_POINT('Ctrl Pts',(182.69989861597,4.81017518725431,333.081484549774));
#6681=CARTESIAN_POINT('Ctrl Pts',(182.655625882176,4.41011242773355,332.360889697057));
#6682=CARTESIAN_POINT('Ctrl Pts',(182.646688201559,4.32214210106214,332.219158160999));
#6683=CARTESIAN_POINT('Ctrl Pts',(182.603520128176,3.86839407895673,331.561802727404));
#6684=CARTESIAN_POINT('Ctrl Pts',(182.56886565616,3.41640076617818,331.112338958661));
#6685=CARTESIAN_POINT('Ctrl Pts',(182.5259497374,2.75657752653948,330.662346682603));
#6686=CARTESIAN_POINT('Ctrl Pts',(182.51702011832,2.6144554422385,330.575231327291));
#6687=CARTESIAN_POINT('Ctrl Pts',(182.472496265327,1.89114024363531,330.178901099645));
#6688=CARTESIAN_POINT('Ctrl Pts',(182.436429323386,1.25847279790753,329.976488090054));
#6689=CARTESIAN_POINT('Ctrl Pts',(182.392100773262,0.439292854233025,329.879353750766));
#6690=CARTESIAN_POINT('Ctrl Pts',(182.383159214547,0.272876512558731,329.867794481007));
#6691=CARTESIAN_POINT('Ctrl Pts',(182.339954928001,-0.526060850280547,329.851274015462));
#6692=CARTESIAN_POINT('Ctrl Pts',(182.305258652713,-1.15534826314823,329.955070004742));
#6693=CARTESIAN_POINT('Ctrl Pts',(182.257553533066,-1.98967609420732,330.257383379467));
#6694=CARTESIAN_POINT('Ctrl Pts',(182.243900241156,-2.22261065129362,330.361980708259));
#6695=CARTESIAN_POINT('Ctrl Pts',(182.209193930791,-2.78260135923999,330.665351934514));
#6696=CARTESIAN_POINT('Ctrl Pts',(182.188206356022,-3.09706803350275,330.884149441227));
#6697=CARTESIAN_POINT('Ctrl Pts',(182.146387628146,-3.67745595577699,331.392464891957));
#6698=CARTESIAN_POINT('Ctrl Pts',(182.125698569782,-3.94038367340356,331.681663211721));
#6699=CARTESIAN_POINT('Ctrl Pts',(182.104574390455,-4.16808369392644,331.997787668581));
#6700=CARTESIAN_POINT('',(182.508202138845,-4.80479214222282,333.183309963564));
#6701=CARTESIAN_POINT('Ctrl Pts',(182.508329008463,-4.80477551437407,333.183318184444));
#6702=CARTESIAN_POINT('Ctrl Pts',(182.493038547972,-4.78161868580243,333.122072807318));
#6703=CARTESIAN_POINT('Ctrl Pts',(182.47705683224,-4.75732077296609,333.061350830662));
#6704=CARTESIAN_POINT('Ctrl Pts',(182.361001743482,-4.58002834629899,332.641628114898));
#6705=CARTESIAN_POINT('Ctrl Pts',(182.237933532832,-4.38798420311668,332.303083772074));
#6706=CARTESIAN_POINT('Ctrl Pts',(182.104574390455,-4.16808369392643,331.997787668581));
#6707=CARTESIAN_POINT('Ctrl Pts',(184.058316793539,-4.81229327647343,336.796673031942));
#6708=CARTESIAN_POINT('Ctrl Pts',(184.031402794846,-4.63905991995926,337.260669375179));
#6709=CARTESIAN_POINT('Ctrl Pts',(184.004066240865,-4.39930198500671,337.698042940383));
#6710=CARTESIAN_POINT('Ctrl Pts',(183.959477777831,-3.89923347510022,338.360509443272));
#6711=CARTESIAN_POINT('Ctrl Pts',(183.941711744794,-3.67329168398738,338.606101798829));
#6712=CARTESIAN_POINT('Ctrl Pts',(183.90579520563,-3.18019378259923,339.04729984871));
#6713=CARTESIAN_POINT('Ctrl Pts',(183.887734091215,-2.91473116938132,339.242476026157));
#6714=CARTESIAN_POINT('Ctrl Pts',(183.833511158755,-2.06243404651175,339.751128071117));
#6715=CARTESIAN_POINT('Ctrl Pts',(183.798761180772,-1.43184871781604,339.977615845926));
#6716=CARTESIAN_POINT('Ctrl Pts',(183.744366530398,-0.449350383568896,340.127693201517));
#6717=CARTESIAN_POINT('Ctrl Pts',(183.726244974851,-0.118996400989805,340.145970270493));
#6718=CARTESIAN_POINT('Ctrl Pts',(183.690771909644,0.539390933238602,340.118924872461));
#6719=CARTESIAN_POINT('Ctrl Pts',(183.673263779812,0.865894535513429,340.073909855269));
#6720=CARTESIAN_POINT('Ctrl Pts',(183.637441117833,1.5097350692145,339.921149051693));
#6721=CARTESIAN_POINT('Ctrl Pts',(183.619198339197,1.8253794029355,339.813001922891));
#6722=CARTESIAN_POINT('Ctrl Pts',(183.564292305223,2.738274016909,339.397408168506));
#6723=CARTESIAN_POINT('Ctrl Pts',(183.529231270503,3.28801853298999,339.00303388018));
#6724=CARTESIAN_POINT('Ctrl Pts',(183.474576098567,3.97208456320005,338.2737527464));
#6725=CARTESIAN_POINT('Ctrl Pts',(183.456424617832,4.17398380994281,338.012106368056));
#6726=CARTESIAN_POINT('Ctrl Pts',(183.421100160243,4.52222629171864,337.457880496178));
#6727=CARTESIAN_POINT('Ctrl Pts',(183.403828819226,4.6685639219126,337.167076686023));
#6728=CARTESIAN_POINT('Ctrl Pts',(183.350579746682,5.02636832228254,336.248490411596));
#6729=CARTESIAN_POINT('Ctrl Pts',(183.314295360742,5.14515622988651,335.592019100404));
#6730=CARTESIAN_POINT('Ctrl Pts',(183.242884447268,5.12729226920193,334.260694268346));
#6731=CARTESIAN_POINT('Ctrl Pts',(183.206240992382,4.98712623354329,333.598502470096));
#6732=CARTESIAN_POINT('Ctrl Pts',(183.15153263591,4.59048297762633,332.670029592873));
#6733=CARTESIAN_POINT('Ctrl Pts',(183.133525660923,4.42662346468804,332.372014283161));
#6734=CARTESIAN_POINT('Ctrl Pts',(183.079457857919,3.85923300195422,331.545696032195));
#6735=CARTESIAN_POINT('Ctrl Pts',(183.042995844251,3.38156985082007,331.076877369247));
#6736=CARTESIAN_POINT('Ctrl Pts',(182.989556769326,2.54990709080552,330.528406180653));
#6737=CARTESIAN_POINT('Ctrl Pts',(182.971703859499,2.25463090722395,330.372494268806));
#6738=CARTESIAN_POINT('Ctrl Pts',(182.935557501039,1.64052021887021,330.121054922684));
#6739=CARTESIAN_POINT('Ctrl Pts',(182.917353750986,1.32332475086542,330.025643806206));
#6740=CARTESIAN_POINT('Ctrl Pts',(182.862335274629,0.330533052436667,329.828771292242));
#6741=CARTESIAN_POINT('Ctrl Pts',(182.826457095763,-0.357862786546009,329.830589265057));
#6742=CARTESIAN_POINT('Ctrl Pts',(182.752296089695,-1.68354853246715,330.100768808326));
#6743=CARTESIAN_POINT('Ctrl Pts',(182.717021322299,-2.30869609605098,330.362463116437));
#6744=CARTESIAN_POINT('Ctrl Pts',(182.652106720335,-3.29831072274798,331.02772756185));
#6745=CARTESIAN_POINT('Ctrl Pts',(182.623532676823,-3.68407824459055,331.382625374769));
#6746=CARTESIAN_POINT('Ctrl Pts',(182.581198022466,-4.17732424866067,331.998669568381));
#6747=CARTESIAN_POINT('Ctrl Pts',(182.566842787961,-4.32819357168361,332.220654920079));
#6748=CARTESIAN_POINT('Ctrl Pts',(182.537698961815,-4.5945884635041,332.687315536805));
#6749=CARTESIAN_POINT('Ctrl Pts',(182.522952343314,-4.70951594817475,332.9313757916));
#6750=CARTESIAN_POINT('Ctrl Pts',(182.508191721177,-4.8047733248247,333.183312393516));
#6751=CARTESIAN_POINT('Origin',(189.09641784506,0.,335.));
#6752=CARTESIAN_POINT('',(182.971417840485,-6.11287942610948,335.000034739551));
#6753=CARTESIAN_POINT('Ctrl Pts',(184.101667378079,3.72297207952785,339.848845683001));
#6754=CARTESIAN_POINT('Ctrl Pts',(184.06577619351,4.35425146681177,339.364145676672));
#6755=CARTESIAN_POINT('Ctrl Pts',(184.028753388829,4.88483466193755,338.760806757196));
#6756=CARTESIAN_POINT('Ctrl Pts',(183.975242140408,5.48153190724963,337.73453769235));
#6757=CARTESIAN_POINT('Ctrl Pts',(183.957754505071,5.64525739647646,337.37822516427));
#6758=CARTESIAN_POINT('Ctrl Pts',(183.921955243047,5.90331852565447,336.636460988997));
#6759=CARTESIAN_POINT('Ctrl Pts',(183.90371825822,5.99652186406069,336.252552776751));
#6760=CARTESIAN_POINT('Ctrl Pts',(183.849244162369,6.16357588372059,335.080159955476));
#6761=CARTESIAN_POINT('Ctrl Pts',(183.814673825568,6.12233986624375,334.283727463203));
#6762=CARTESIAN_POINT('Ctrl Pts',(183.76030572938,5.83597727670729,333.138361590064));
#6763=CARTESIAN_POINT('Ctrl Pts',(183.742219507261,5.70516911181519,332.769440905078));
#6764=CARTESIAN_POINT('Ctrl Pts',(183.707033966877,5.37616921254842,332.064201434522));
#6765=CARTESIAN_POINT('Ctrl Pts',(183.689753551581,5.17923231673713,331.72927171304));
#6766=CARTESIAN_POINT('Ctrl Pts',(183.654152583233,4.71968857120385,331.094466222427));
#6767=CARTESIAN_POINT('Ctrl Pts',(183.635893744349,4.45685056697839,330.797010174992));
#6768=CARTESIAN_POINT('Ctrl Pts',(183.580774235543,3.58212912876583,329.982093757339));
#6769=CARTESIAN_POINT('Ctrl Pts',(183.545795551112,2.89589044099009,329.557127752101));
#6770=CARTESIAN_POINT('Ctrl Pts',(183.49110700814,1.78201204891041,329.139240876818));
#6771=CARTESIAN_POINT('Ctrl Pts',(183.472983860139,1.40440778926222,329.037474092261));
#6772=CARTESIAN_POINT('Ctrl Pts',(183.429381363174,0.457065736262491,328.877213822844));
#6773=CARTESIAN_POINT('Ctrl Pts',(183.404099041264,-0.116111425258274,328.861274384291));
#6774=CARTESIAN_POINT('Ctrl Pts',(183.3600040241,-1.0717100492714,328.968736056802));
#6775=CARTESIAN_POINT('Ctrl Pts',(183.341838260232,-1.45516963137122,329.04960635248));
#6776=CARTESIAN_POINT('Ctrl Pts',(183.301857700579,-2.29133659393769,329.311670256026));
#6777=CARTESIAN_POINT('Ctrl Pts',(183.280383262249,-2.73548133766137,329.511423189919));
#6778=CARTESIAN_POINT('Ctrl Pts',(183.240332694653,-3.49026222444738,329.965484366751));
#6779=CARTESIAN_POINT('Ctrl Pts',(183.22207706571,-3.80860591688538,330.201793487443));
#6780=CARTESIAN_POINT('Ctrl Pts',(183.167072252517,-4.69356128800703,331.002615052679));
#6781=CARTESIAN_POINT('Ctrl Pts',(183.132167029559,-5.17471703029592,331.648744745133));
#6782=CARTESIAN_POINT('Ctrl Pts',(183.074871172973,-5.71081509644631,332.773154926883));
#6783=CARTESIAN_POINT('Ctrl Pts',(183.054135616454,-5.8585197077799,333.197218323336));
#6784=CARTESIAN_POINT('Ctrl Pts',(183.013181414721,-6.06137256395018,334.081822709202));
#6785=CARTESIAN_POINT('Ctrl Pts',(182.992662680761,-6.11325334319966,334.540200001429));
#6786=CARTESIAN_POINT('Ctrl Pts',(182.971631360442,-6.11324999983842,335.000044447211));
#6787=CARTESIAN_POINT('Ctrl Pts',(182.971417840484,-6.11287942610948,335.000034739551));
#6788=CARTESIAN_POINT('Ctrl Pts',(182.951327947679,-6.1130202861597,335.441078492841));
#6789=CARTESIAN_POINT('Ctrl Pts',(182.885455337599,-5.95859552868657,336.887118858306));
#6790=CARTESIAN_POINT('Ctrl Pts',(182.773800010244,-4.83029117599585,339.147696732808));
#6791=CARTESIAN_POINT('Ctrl Pts',(182.63645185842,-2.29132112187004,340.94001112084));
#6792=CARTESIAN_POINT('Ctrl Pts',(182.499103706597,0.793490165733074,341.316971685497));
#6793=CARTESIAN_POINT('Ctrl Pts',(182.40413033467,2.79592192577249,340.536520946628));
#6794=CARTESIAN_POINT('Ctrl Pts',(182.354939680017,3.66377807797318,339.894536771844));
#6795=CARTESIAN_POINT('Ctrl Pts',(182.351531742639,3.72305791812513,339.848957366357));
#6796=CARTESIAN_POINT('Ctrl Pts',(182.497067674234,3.72297189708705,339.84884582308));
#6797=CARTESIAN_POINT('Ctrl Pts',(182.506942057296,3.54913485701041,339.982318908943));
#6798=CARTESIAN_POINT('Ctrl Pts',(182.51684541491,3.36801225584443,340.106526560382));
#6799=CARTESIAN_POINT('Ctrl Pts',(182.544634213801,2.84640571252878,340.424268096816));
#6800=CARTESIAN_POINT('Ctrl Pts',(182.56266887492,2.49373645185283,340.595174463556));
#6801=CARTESIAN_POINT('Ctrl Pts',(182.598653591292,1.76007502943536,340.867477519029));
#6802=CARTESIAN_POINT('Ctrl Pts',(182.61622231947,1.38073110582571,340.968144057333));
#6803=CARTESIAN_POINT('Ctrl Pts',(182.669676867992,0.211030556525817,341.160972236312));
#6804=CARTESIAN_POINT('Ctrl Pts',(182.70645653674,-0.589998681150672,341.136286509658));
#6805=CARTESIAN_POINT('Ctrl Pts',(182.760155597291,-1.74930998512255,340.870951182526));
#6806=CARTESIAN_POINT('Ctrl Pts',(182.77785545865,-2.12525767241027,340.745557508671));
#6807=CARTESIAN_POINT('Ctrl Pts',(182.813596937793,-2.84112731345366,340.426835855446));
#6808=CARTESIAN_POINT('Ctrl Pts',(182.831545415987,-3.17994840794276,340.235501035293));
#6809=CARTESIAN_POINT('Ctrl Pts',(182.867286529096,-3.81873547811517,339.789753689841));
#6810=CARTESIAN_POINT('Ctrl Pts',(182.884744271952,-4.11697244107476,339.535969791996));
#6811=CARTESIAN_POINT('Ctrl Pts',(182.938488550358,-4.94564300042357,338.681304238242));
#6812=CARTESIAN_POINT('Ctrl Pts',(182.975538596472,-5.38429373502866,338.003459523774));
#6813=CARTESIAN_POINT('Ctrl Pts',(183.029479066173,-5.8267361261942,336.891682844458));
#6814=CARTESIAN_POINT('Ctrl Pts',(183.047298692267,-5.93721977410194,336.509547483994));
#6815=CARTESIAN_POINT('Ctrl Pts',(183.083905818102,-6.08379936212537,335.72259216024));
#6816=CARTESIAN_POINT('Ctrl Pts',(183.102617773177,-6.11822770455929,335.319433322501));
#6817=CARTESIAN_POINT('Ctrl Pts',(183.13888783016,-6.10728751354646,334.524875739508));
#6818=CARTESIAN_POINT('Ctrl Pts',(183.156305159263,-6.06440909376596,334.135330725164));
#6819=CARTESIAN_POINT('Ctrl Pts',(183.21019802125,-5.82148314915544,332.969894819936));
#6820=CARTESIAN_POINT('Ctrl Pts',(183.247141359612,-5.5063884631937,332.226792200719));
#6821=CARTESIAN_POINT('Ctrl Pts',(183.319668521704,-4.6017562250993,330.894774932291));
#6822=CARTESIAN_POINT('Ctrl Pts',(183.357053550118,-4.01740774154997,330.321384832669));
#6823=CARTESIAN_POINT('Ctrl Pts',(183.411619846854,-3.00884645031306,329.663961180505));
#6824=CARTESIAN_POINT('Ctrl Pts',(183.429169468911,-2.65945790878523,329.48150794177));
#6825=CARTESIAN_POINT('Ctrl Pts',(183.464868374054,-1.93143117386542,329.186632514181));
#6826=CARTESIAN_POINT('Ctrl Pts',(183.482937768214,-1.55456821070283,329.074717421328));
#6827=CARTESIAN_POINT('Ctrl Pts',(183.537703942053,-0.386455172397558,328.847025209151));
#6828=CARTESIAN_POINT('Ctrl Pts',(183.572741573386,0.419044494804354,328.849158734953));
#6829=CARTESIAN_POINT('Ctrl Pts',(183.627441193638,1.5849296429038,329.082834237044));
#6830=CARTESIAN_POINT('Ctrl Pts',(183.645494368152,1.96023768523414,329.196351183364));
#6831=CARTESIAN_POINT('Ctrl Pts',(183.68079565119,2.68291193061905,329.49310217574));
#6832=CARTESIAN_POINT('Ctrl Pts',(183.698241466175,3.02869057786356,329.675436834926));
#6833=CARTESIAN_POINT('Ctrl Pts',(183.733980331057,3.6844885044124,330.105925853116));
#6834=CARTESIAN_POINT('Ctrl Pts',(183.752201849441,3.99251437679522,330.353793380723));
#6835=CARTESIAN_POINT('Ctrl Pts',(183.806480331159,4.83747867651192,331.180215283661));
#6836=CARTESIAN_POINT('Ctrl Pts',(183.84109938916,5.28879016709082,331.83445910563));
#6837=CARTESIAN_POINT('Ctrl Pts',(183.886472648189,5.68270280946381,332.737723543505));
#6838=CARTESIAN_POINT('Ctrl Pts',(183.895608100515,5.75296897842462,332.922897617365));
#6839=CARTESIAN_POINT('Ctrl Pts',(183.941859290831,6.06453728829434,333.881947657604));
#6840=CARTESIAN_POINT('Ctrl Pts',(183.977540424845,6.15918472154949,334.694892606177));
#6841=CARTESIAN_POINT('Ctrl Pts',(184.024025798513,6.07624292445715,335.700330900127));
#6842=CARTESIAN_POINT('Ctrl Pts',(184.033175274057,6.05031410281653,335.897157616979));
#6843=CARTESIAN_POINT('Ctrl Pts',(184.060675687534,5.94278233206975,336.489251283774));
#6844=CARTESIAN_POINT('Ctrl Pts',(184.078635082676,5.83160136248364,336.878020796191));
#6845=CARTESIAN_POINT('Ctrl Pts',(184.132599901332,5.39230653803588,337.98609184279));
#6846=CARTESIAN_POINT('Ctrl Pts',(184.169066451217,4.96255223853182,338.656062637848));
#6847=CARTESIAN_POINT('Ctrl Pts',(184.218649363363,4.2016545045412,339.451443104235));
#6848=CARTESIAN_POINT('Ctrl Pts',(184.232676234344,3.96942652186749,339.659616522155));
#6849=CARTESIAN_POINT('Ctrl Pts',(184.246855413009,3.72297205899967,339.848845698762));
#6850=CARTESIAN_POINT('Origin',(180.696454890107,-1.2379162167118E-15,335.));
#6851=CARTESIAN_POINT('',(180.696454890107,3.31445696909756,340.13675));
#6852=CARTESIAN_POINT('',(180.696492164137,-2.55835334313229,340.136710345109));
#6853=CARTESIAN_POINT('',(180.696454890107,0.,340.13675));
#6854=CARTESIAN_POINT('',(180.696454890107,1.88832481980914,340.814297458627));
#6855=CARTESIAN_POINT('Origin',(180.696454890107,0.,335.));
#6856=CARTESIAN_POINT('Ctrl Pts',(180.696454890107,1.88832481980918,340.814297458627));
#6857=CARTESIAN_POINT('Ctrl Pts',(180.696454890107,1.72234987206334,340.854084373528));
#6858=CARTESIAN_POINT('Ctrl Pts',(180.696454890107,1.55490266737403,340.886650186877));
#6859=CARTESIAN_POINT('Ctrl Pts',(180.696454890107,1.38643951722482,340.912046446392));
#6860=CARTESIAN_POINT('Ctrl Pts',(180.696454890107,1.21798855966071,340.937440867843));
#6861=CARTESIAN_POINT('Ctrl Pts',(180.696454890107,1.04852103763536,340.955666657136));
#6862=CARTESIAN_POINT('Ctrl Pts',(180.696454890107,0.878495083065094,340.966723276416));
#6863=CARTESIAN_POINT('Ctrl Pts',(180.696454890106,0.782313019899616,340.972977900639));
#6864=CARTESIAN_POINT('Ctrl Pts',(180.696454890107,0.685952353875762,340.976937415162));
#6865=CARTESIAN_POINT('Ctrl Pts',(180.696454890106,0.589497696366717,340.97859454858));
#6866=CARTESIAN_POINT('Ctrl Pts',(180.696454890106,0.545379466010032,340.979352519172));
#6867=CARTESIAN_POINT('Ctrl Pts',(180.696454890107,0.501241594199461,340.979628729878));
#6868=CARTESIAN_POINT('Ctrl Pts',(180.696454890106,0.457092311071317,340.979422130108));
#6869=CARTESIAN_POINT('Ctrl Pts',(180.696454890106,0.428525290762674,340.979288448665));
#6870=CARTESIAN_POINT('Ctrl Pts',(180.696454890107,0.399960654754582,340.978952617827));
#6871=CARTESIAN_POINT('Ctrl Pts',(180.696454890107,0.371408088900426,340.978414853351));
#6872=CARTESIAN_POINT('Ctrl Pts',(180.696454890107,0.203593320499692,340.975254197965));
#6873=CARTESIAN_POINT('Ctrl Pts',(180.696454890106,0.0361136110770114,340.965121784186));
#6874=CARTESIAN_POINT('Ctrl Pts',(180.696454890106,-0.130589187275098,340.948025867259));
#6875=CARTESIAN_POINT('Ctrl Pts',(180.696454890106,-0.296170731460119,340.931044938613));
#6876=CARTESIAN_POINT('Ctrl Pts',(180.696454890106,-0.460986474971263,340.907193694938));
#6877=CARTESIAN_POINT('Ctrl Pts',(180.696454890106,-0.624587627822799,340.876431826722));
#6878=CARTESIAN_POINT('Ctrl Pts',(180.696454890106,-0.690380933313477,340.864060734235));
#6879=CARTESIAN_POINT('Ctrl Pts',(180.696454890107,-0.755977566272227,340.850571450757));
#6880=CARTESIAN_POINT('Ctrl Pts',(180.696454890107,-0.821347224492345,340.835959217821));
#6881=CARTESIAN_POINT('Ctrl Pts',(180.696454890107,-0.857644271323373,340.827845653858));
#6882=CARTESIAN_POINT('Ctrl Pts',(180.696454890107,-0.893871326317157,340.819385849771));
#6883=CARTESIAN_POINT('Ctrl Pts',(180.696454890107,-0.930023097778579,340.810578830702));
#6884=CARTESIAN_POINT('Ctrl Pts',(180.696454890107,-0.957697296363754,340.803837053334));
#6885=CARTESIAN_POINT('Ctrl Pts',(180.696454890107,-0.985330455584287,340.796890932872));
#6886=CARTESIAN_POINT('Ctrl Pts',(180.696454890106,-1.01289593960887,340.789746501884));
#6887=CARTESIAN_POINT('Ctrl Pts',(180.696454890106,-1.14387746377719,340.755798668453));
#6888=CARTESIAN_POINT('Ctrl Pts',(180.696454890106,-1.27344265908636,340.71734924744));
#6889=CARTESIAN_POINT('Ctrl Pts',(180.696454890106,-1.40136267565137,340.674406381647));
#6890=CARTESIAN_POINT('Ctrl Pts',(180.696454890106,-1.55702980066537,340.622148786336));
#6891=CARTESIAN_POINT('Ctrl Pts',(180.696454890106,-1.71026170156066,340.563238091871));
#6892=CARTESIAN_POINT('Ctrl Pts',(180.696454890106,-1.86067649098094,340.497921756323));
#6893=CARTESIAN_POINT('Ctrl Pts',(180.696454890106,-2.01048424259179,340.43286902175));
#6894=CARTESIAN_POINT('Ctrl Pts',(180.696454890106,-2.15749817695002,340.361461748611));
#6895=CARTESIAN_POINT('Ctrl Pts',(180.696454890106,-2.30131165414403,340.283902230785));
#6896=CARTESIAN_POINT('Ctrl Pts',(180.696454890106,-2.38812811128342,340.237081566363));
#6897=CARTESIAN_POINT('Ctrl Pts',(180.696454890106,-2.47377764295648,340.18801810646));
#6898=CARTESIAN_POINT('Ctrl Pts',(180.696454890107,-2.55816418736645,340.13675));
#6899=CARTESIAN_POINT('Ctrl Pts',(185.231465761173,-1.57897629365943,329.093805880512));
#6900=CARTESIAN_POINT('Ctrl Pts',(185.187526654506,-2.51072920729258,329.342902969502));
#6901=CARTESIAN_POINT('Ctrl Pts',(185.099648441175,-4.25344831580121,330.290005670493));
#6902=CARTESIAN_POINT('Ctrl Pts',(184.96783112118,-5.93304968749718,332.746577952619));
#6903=CARTESIAN_POINT('Ctrl Pts',(184.836013801182,-6.30803335278088,335.698484020827));
#6904=CARTESIAN_POINT('Ctrl Pts',(184.704196481186,-5.29636932799949,338.49694942919));
#6905=CARTESIAN_POINT('Ctrl Pts',(184.572379161188,-3.12028812894157,340.526647782566));
#6906=CARTESIAN_POINT('Ctrl Pts',(184.440561841193,-0.258262683773776,341.341399014455));
#6907=CARTESIAN_POINT('Ctrl Pts',(184.308744521195,2.66055317911897,340.762062281473));
#6908=CARTESIAN_POINT('Ctrl Pts',(184.176927201199,4.99446944125117,338.916002801078));
#6909=CARTESIAN_POINT('Ctrl Pts',(184.045109881202,6.23040426257297,336.209052024929));
#6910=CARTESIAN_POINT('Ctrl Pts',(183.913292561205,6.09664594605466,333.236306302429));
#6911=CARTESIAN_POINT('Ctrl Pts',(183.781475241208,4.62260115430969,330.651292619679));
#6912=CARTESIAN_POINT('Ctrl Pts',(183.649657921213,2.13232327726643,329.022300393848));
#6913=CARTESIAN_POINT('Ctrl Pts',(183.517840601215,-0.826724487129161,328.707446948171));
#6914=CARTESIAN_POINT('Ctrl Pts',(183.386023281219,-3.60402487195393,329.775949553599));
#6915=CARTESIAN_POINT('Ctrl Pts',(183.254205961221,-5.58901576521575,331.992908371219));
#6916=CARTESIAN_POINT('Ctrl Pts',(183.122388641226,-6.34531641714774,334.870946885228));
#6917=CARTESIAN_POINT('Ctrl Pts',(182.990571321228,-5.70666151580543,337.777356955005));
#6918=CARTESIAN_POINT('Ctrl Pts',(182.858754001232,-3.81345246746879,340.073193030899));
#6919=CARTESIAN_POINT('Ctrl Pts',(182.726936681235,-1.081892576986,341.253739083616));
#6920=CARTESIAN_POINT('Ctrl Pts',(182.595119361239,1.88751380770297,341.05946322403));
#6921=CARTESIAN_POINT('Ctrl Pts',(182.463302041241,4.4419707709344,339.533078493106));
#6922=CARTESIAN_POINT('Ctrl Pts',(182.331484721246,6.01991459103887,337.010141634552));
#6923=CARTESIAN_POINT('Ctrl Pts',(182.199667401248,6.27444029061672,334.045310123841));
#6924=CARTESIAN_POINT('Ctrl Pts',(182.067850081252,5.14962919993828,331.290350087674));
#6925=CARTESIAN_POINT('Ctrl Pts',(181.936032761254,2.89270329319507,329.350979521661));
#6926=CARTESIAN_POINT('Ctrl Pts',(181.804215441259,-8.68525194521966E-6,
328.653426946938));
#6927=CARTESIAN_POINT('Ctrl Pts',(181.672392861162,-2.89299401697966,329.351388838593));
#6928=CARTESIAN_POINT('Ctrl Pts',(181.584509387731,-4.39722124418262,330.644407214387));
#6929=CARTESIAN_POINT('Ctrl Pts',(181.540565020965,-4.96093856271488,331.427132287955));
#6930=CARTESIAN_POINT('Ctrl Pts',(185.419558053325,-1.49483501435035,329.408538109904));
#6931=CARTESIAN_POINT('Ctrl Pts',(185.37561894666,-2.37693621220545,329.644361188497));
#6932=CARTESIAN_POINT('Ctrl Pts',(185.287740733328,-4.02678843230346,330.540994206556));
#6933=CARTESIAN_POINT('Ctrl Pts',(185.155923413332,-5.61688636515029,332.866659434938));
#6934=CARTESIAN_POINT('Ctrl Pts',(185.024106093335,-5.971887713129,335.661262854603));
#6935=CARTESIAN_POINT('Ctrl Pts',(184.892288773338,-5.01413374742697,338.310602237131));
#6936=CARTESIAN_POINT('Ctrl Pts',(184.760471453342,-2.95401265283952,340.232141008409));
#6937=CARTESIAN_POINT('Ctrl Pts',(184.628654133345,-0.244500252572128,341.003475368718));
#6938=CARTESIAN_POINT('Ctrl Pts',(184.496836813348,2.51877628920628,340.45501062163));
#6939=CARTESIAN_POINT('Ctrl Pts',(184.365019493352,4.72832165300097,338.707324883124));
#6940=CARTESIAN_POINT('Ctrl Pts',(184.233202173355,5.89839536074794,336.144623455269));
#6941=CARTESIAN_POINT('Ctrl Pts',(184.101384853358,5.77176482437128,333.330290895243));
#6942=CARTESIAN_POINT('Ctrl Pts',(183.969567533362,4.37626966952355,330.883028715902));
#6943=CARTESIAN_POINT('Ctrl Pts',(183.837750213365,2.01869496684138,329.340843043416));
#6944=CARTESIAN_POINT('Ctrl Pts',(183.705932893368,-0.782669578729003,329.042767665794));
#6945=CARTESIAN_POINT('Ctrl Pts',(183.574115573371,-3.41197179008965,330.0543313694));
#6946=CARTESIAN_POINT('Ctrl Pts',(183.442298253375,-5.29118549477264,332.153151775544));
#6947=CARTESIAN_POINT('Ctrl Pts',(183.310480933378,-6.00718401889474,334.877823932224));
#6948=CARTESIAN_POINT('Ctrl Pts',(183.178663613381,-5.40256207970122,337.629355767001));
#6949=CARTESIAN_POINT('Ctrl Pts',(183.046846293385,-3.61023930303708,339.802850180587));
#6950=CARTESIAN_POINT('Ctrl Pts',(182.915028973388,-1.02424014365426,340.920486704163));
#6951=CARTESIAN_POINT('Ctrl Pts',(182.783211653391,1.78693102686489,340.736563513855));
#6952=CARTESIAN_POINT('Ctrl Pts',(182.651394333395,4.20526480845682,339.291517536713));
#6953=CARTESIAN_POINT('Ctrl Pts',(182.519577013398,5.69912236821994,336.903024200679));
#6954=CARTESIAN_POINT('Ctrl Pts',(182.387759693401,5.94008477488104,334.096184115962));
#6955=CARTESIAN_POINT('Ctrl Pts',(182.255942373404,4.87521318078071,331.488031769574));
#6956=CARTESIAN_POINT('Ctrl Pts',(182.124125053408,2.738555471769,329.652007353302));
#6957=CARTESIAN_POINT('Ctrl Pts',(181.992307733411,-8.22242789026327E-6,
328.991626309435));
#6958=CARTESIAN_POINT('Ctrl Pts',(181.860485153315,-2.73883070331901,329.652394858347));
#6959=CARTESIAN_POINT('Ctrl Pts',(181.772601679884,-4.16289991689208,330.876510223535));
#6960=CARTESIAN_POINT('Ctrl Pts',(181.728657313119,-4.69657758470859,331.617525051482));
#6961=CARTESIAN_POINT('Ctrl Pts',(185.607650345478,-1.41069373504128,329.723270339297));
#6962=CARTESIAN_POINT('Ctrl Pts',(185.563711238813,-2.24314321711833,329.945819407492));
#6963=CARTESIAN_POINT('Ctrl Pts',(185.475833025482,-3.80012854880572,330.791982742619));
#6964=CARTESIAN_POINT('Ctrl Pts',(185.344015705485,-5.30072304280342,332.986740917257));
#6965=CARTESIAN_POINT('Ctrl Pts',(185.212198385488,-5.63574207347713,335.62404168838));
#6966=CARTESIAN_POINT('Ctrl Pts',(185.080381065492,-4.73189816685444,338.124255045072));
#6967=CARTESIAN_POINT('Ctrl Pts',(184.948563745495,-2.78773717673747,339.937634234253));
#6968=CARTESIAN_POINT('Ctrl Pts',(184.816746425498,-0.230737821370482,340.665551722981));
#6969=CARTESIAN_POINT('Ctrl Pts',(184.684929105501,2.37699939929359,340.147958961786));
#6970=CARTESIAN_POINT('Ctrl Pts',(184.553111785505,4.46217386475077,338.49864696517));
#6971=CARTESIAN_POINT('Ctrl Pts',(184.421294465508,5.56638645892292,336.080194885608));
#6972=CARTESIAN_POINT('Ctrl Pts',(184.289477145511,5.44688370268791,333.424275488058));
#6973=CARTESIAN_POINT('Ctrl Pts',(184.157659825515,4.12993818473742,331.114764812125));
#6974=CARTESIAN_POINT('Ctrl Pts',(184.025842505518,1.90506665641634,329.659385692984));
#6975=CARTESIAN_POINT('Ctrl Pts',(183.894025185521,-0.738614670328843,329.378088383418));
#6976=CARTESIAN_POINT('Ctrl Pts',(183.762207865525,-3.21991870822537,330.332713185201));
#6977=CARTESIAN_POINT('Ctrl Pts',(183.630390545528,-4.99335522432953,332.313395179871));
#6978=CARTESIAN_POINT('Ctrl Pts',(183.498573225531,-5.66905162064175,334.884700979218));
#6979=CARTESIAN_POINT('Ctrl Pts',(183.366755905535,-5.09846264359701,337.481354578996));
#6980=CARTESIAN_POINT('Ctrl Pts',(183.234938585538,-3.40702613860538,339.532507330276));
#6981=CARTESIAN_POINT('Ctrl Pts',(183.103121265541,-0.966587710322523,340.587234324711));
#6982=CARTESIAN_POINT('Ctrl Pts',(182.971303945544,1.68634824602681,340.41366380368));
#6983=CARTESIAN_POINT('Ctrl Pts',(182.839486625548,3.96855884597923,339.04995658032));
#6984=CARTESIAN_POINT('Ctrl Pts',(182.707669305551,5.37833014540103,336.795906766805));
#6985=CARTESIAN_POINT('Ctrl Pts',(182.575851985554,5.60572925914536,334.147058108084));
#6986=CARTESIAN_POINT('Ctrl Pts',(182.444034665558,4.60079716162315,331.685713451475));
#6987=CARTESIAN_POINT('Ctrl Pts',(182.312217345561,2.58440765034293,329.953035184941));
#6988=CARTESIAN_POINT('Ctrl Pts',(182.180400025564,-7.75960383703391E-6,
329.329825671931));
#6989=CARTESIAN_POINT('Ctrl Pts',(182.048577445467,-2.58466738965833,329.953400878101));
#6990=CARTESIAN_POINT('Ctrl Pts',(181.960693972037,-3.92857858960154,331.108613232682));
#6991=CARTESIAN_POINT('Ctrl Pts',(181.916749605272,-4.4322166067023,331.807917815009));
#6992=CARTESIAN_POINT('Ctrl Pts',(185.795742637632,-1.3265524557322,330.03800256869));
#6993=CARTESIAN_POINT('Ctrl Pts',(185.751803530966,-2.1093502220312,330.247277626486));
#6994=CARTESIAN_POINT('Ctrl Pts',(185.663925317635,-3.57346866530796,331.042971278682));
#6995=CARTESIAN_POINT('Ctrl Pts',(185.532107997638,-4.98455972045654,333.106822399577));
#6996=CARTESIAN_POINT('Ctrl Pts',(185.400290677642,-5.29959643382524,335.586820522156));
#6997=CARTESIAN_POINT('Ctrl Pts',(185.268473357645,-4.44966258628191,337.937907853013));
#6998=CARTESIAN_POINT('Ctrl Pts',(185.136656037648,-2.62146170063543,339.643127460095));
#6999=CARTESIAN_POINT('Ctrl Pts',(185.004838717651,-0.216975390168832,340.327628077244));
#7000=CARTESIAN_POINT('Ctrl Pts',(184.873021397655,2.23522250938089,339.840907301943));
#7001=CARTESIAN_POINT('Ctrl Pts',(184.741204077658,4.19602607650056,338.289969047214));
#7002=CARTESIAN_POINT('Ctrl Pts',(184.609386757661,5.2343775570979,336.015766315947));
#7003=CARTESIAN_POINT('Ctrl Pts',(184.477569437665,5.12200258100453,333.518260080872));
#7004=CARTESIAN_POINT('Ctrl Pts',(184.345752117668,3.88360669995128,331.346500908347));
#7005=CARTESIAN_POINT('Ctrl Pts',(184.213934797671,1.79143834599129,329.977928342551));
#7006=CARTESIAN_POINT('Ctrl Pts',(184.082117477675,-0.694559761928685,329.713409101043));
#7007=CARTESIAN_POINT('Ctrl Pts',(183.950300157678,-3.02786562636109,330.611095001001));
#7008=CARTESIAN_POINT('Ctrl Pts',(183.818482837681,-4.69552495388641,332.473638584196));
#7009=CARTESIAN_POINT('Ctrl Pts',(183.686665517684,-5.33091922238874,334.891578026213));
#7010=CARTESIAN_POINT('Ctrl Pts',(183.554848197688,-4.79436320749281,337.333353390992));
#7011=CARTESIAN_POINT('Ctrl Pts',(183.423030877691,-3.20381297417367,339.262164479964));
#7012=CARTESIAN_POINT('Ctrl Pts',(183.291213557694,-0.908935276990783,340.253981945258));
#7013=CARTESIAN_POINT('Ctrl Pts',(183.159396237698,1.58576546518872,340.090764093505));
#7014=CARTESIAN_POINT('Ctrl Pts',(183.027578917701,3.73185288350165,338.808395623926));
#7015=CARTESIAN_POINT('Ctrl Pts',(182.895761597704,5.05753792258211,336.688789332932));
#7016=CARTESIAN_POINT('Ctrl Pts',(182.763944277708,5.27137374340969,334.197932100204));
#7017=CARTESIAN_POINT('Ctrl Pts',(182.632126957711,4.32638114246559,331.883395133376));
#7018=CARTESIAN_POINT('Ctrl Pts',(182.500309637714,2.43025982891686,330.25406301658));
#7019=CARTESIAN_POINT('Ctrl Pts',(182.368492317717,-7.2967797819764E-6,
329.668025034428));
#7020=CARTESIAN_POINT('Ctrl Pts',(182.236669737621,-2.43050407599766,330.254406897855));
#7021=CARTESIAN_POINT('Ctrl Pts',(182.148786264191,-3.694257262311,331.340716241829));
#7022=CARTESIAN_POINT('Ctrl Pts',(182.104841897425,-4.16785562869599,331.998310578537));
#7023=CARTESIAN_POINT('',(182.098201455916,5.31714584066979,331.98324026125));
#7024=CARTESIAN_POINT('Ctrl Pts',(182.098201455916,5.31714584066979,331.98324026125));
#7025=CARTESIAN_POINT('Ctrl Pts',(182.36457224063,5.17153456945061,332.589533674022));
#7026=CARTESIAN_POINT('Ctrl Pts',(182.554272439508,5.16167093112009,333.243177234899));
#7027=CARTESIAN_POINT('Ctrl Pts',(182.670936690558,5.19563211857749,334.03882223056));
#7028=CARTESIAN_POINT('Ctrl Pts',(182.68630128761,5.2025413294724,334.166354142561));
#7029=CARTESIAN_POINT('Ctrl Pts',(182.703702995273,5.21403594167573,334.350346852869));
#7030=CARTESIAN_POINT('Ctrl Pts',(182.708406884636,5.21778458694108,334.406932672582));
#7031=CARTESIAN_POINT('Ctrl Pts',(182.714388202159,5.22360384695214,334.490341292768));
#7032=CARTESIAN_POINT('Ctrl Pts',(182.716165632488,5.22551862931197,334.517145465015));
#7033=CARTESIAN_POINT('Ctrl Pts',(182.718501948241,5.22832067126957,334.555496791075));
#7034=CARTESIAN_POINT('Ctrl Pts',(182.719178355383,5.2291721325378,334.567040032337));
#7035=CARTESIAN_POINT('Ctrl Pts',(182.720301290642,5.23065780095879,334.586993502636));
#7036=CARTESIAN_POINT('Ctrl Pts',(182.720760367791,5.23128822200705,334.595403370524));
#7037=CARTESIAN_POINT('Ctrl Pts',(182.721612623099,5.23250403548237,334.611514451517));
#7038=CARTESIAN_POINT('Ctrl Pts',(182.722008094904,5.23308874225913,334.619215625598));
#7039=CARTESIAN_POINT('Ctrl Pts',(182.722906943869,5.2344672066849,334.637262610451));
#7040=CARTESIAN_POINT('Ctrl Pts',(182.723400757176,5.23526382239148,334.647608723816));
#7041=CARTESIAN_POINT('Ctrl Pts',(182.725084299949,5.23812572066465,334.684485286556));
#7042=CARTESIAN_POINT('Ctrl Pts',(182.726154441246,5.24022647461265,334.711018977282));
#7043=CARTESIAN_POINT('Ctrl Pts',(182.729082371591,5.2469763856141,334.794640030317));
#7044=CARTESIAN_POINT('Ctrl Pts',(182.730428556705,5.25177509506523,334.85173840005));
#7045=CARTESIAN_POINT('Ctrl Pts',(182.732688615482,5.2680118439349,335.037633251014));
#7046=CARTESIAN_POINT('Ctrl Pts',(182.730932937796,5.28021507889153,335.166443779557));
#7047=CARTESIAN_POINT('Ctrl Pts',(182.696705720863,5.36952673614242,336.03602657289));
#7048=CARTESIAN_POINT('Ctrl Pts',(182.558201552268,5.47160557667786,336.732739156913));
#7049=CARTESIAN_POINT('Ctrl Pts',(182.352165757496,5.64138616135816,337.35555453857));
#7050=CARTESIAN_POINT('',(181.566511620574,-4.60983126052084,330.984868456448));
#7051=CARTESIAN_POINT('Ctrl Pts',(182.098194326107,5.31700541326403,331.983167389824));
#7052=CARTESIAN_POINT('Ctrl Pts',(182.090071372961,5.22902379605754,331.82810451581));
#7053=CARTESIAN_POINT('Ctrl Pts',(182.081948419816,5.13427134210817,331.676921153739));
#7054=CARTESIAN_POINT('Ctrl Pts',(182.073825466671,5.03310363410748,331.53017387023));
#7055=CARTESIAN_POINT('Ctrl Pts',(182.071904021973,5.00917290933089,331.49546152058));
#7056=CARTESIAN_POINT('Ctrl Pts',(182.069982577276,4.98488341958961,331.460997258886));
#7057=CARTESIAN_POINT('Ctrl Pts',(182.068061132578,4.96024022379589,331.426788211603));
#7058=CARTESIAN_POINT('Ctrl Pts',(182.060324476436,4.86101492090906,331.28904621148));
#7059=CARTESIAN_POINT('Ctrl Pts',(182.052587820295,4.75603357271204,331.155418986902));
#7060=CARTESIAN_POINT('Ctrl Pts',(182.044851164153,4.64566163367922,331.026380296523));
#7061=CARTESIAN_POINT('Ctrl Pts',(182.037115822775,4.5353084512093,330.897363534927));
#7062=CARTESIAN_POINT('Ctrl Pts',(182.029380481398,4.41956671061087,330.772933990555));
#7063=CARTESIAN_POINT('Ctrl Pts',(182.02164514002,4.29884172136742,330.65353184561));
#7064=CARTESIAN_POINT('Ctrl Pts',(182.013909513125,4.17811227606205,330.534125293429));
#7065=CARTESIAN_POINT('Ctrl Pts',(182.00617388623,4.0523994357841,330.419746735568));
#7066=CARTESIAN_POINT('Ctrl Pts',(181.998438259334,3.92214543589988,330.310799562596));
#7067=CARTESIAN_POINT('Ctrl Pts',(181.990703046904,3.79189841486783,330.201858226882));
#7068=CARTESIAN_POINT('Ctrl Pts',(181.982967834474,3.65711096304351,330.098347895273));
#7069=CARTESIAN_POINT('Ctrl Pts',(181.975232622044,3.51825864005062,330.000631869505));
#7070=CARTESIAN_POINT('Ctrl Pts',(181.967495806112,3.37937753310672,329.902895587301));
#7071=CARTESIAN_POINT('Ctrl Pts',(181.959758990181,3.23643012848004,329.810956192851));
#7072=CARTESIAN_POINT('Ctrl Pts',(181.952022174249,3.08992193242528,329.725134313178));
#7073=CARTESIAN_POINT('Ctrl Pts',(181.946762720359,2.99032629665983,329.666792971882));
#7074=CARTESIAN_POINT('Ctrl Pts',(181.94150326647,2.88908575465452,329.61127777646));
#7075=CARTESIAN_POINT('Ctrl Pts',(181.936243812581,2.78636597990251,329.558677533123));
#7076=CARTESIAN_POINT('Ctrl Pts',(181.92850168363,2.63515831487129,329.481247846441));
#7077=CARTESIAN_POINT('Ctrl Pts',(181.92075955468,2.48069895433928,329.410113469557));
#7078=CARTESIAN_POINT('Ctrl Pts',(181.913017425729,2.32352993282106,329.34552971413));
#7079=CARTESIAN_POINT('Ctrl Pts',(181.905276596609,2.16638729849708,329.280956801706));
#7080=CARTESIAN_POINT('Ctrl Pts',(181.897535767488,2.00653620131673,329.22293243518));
#7081=CARTESIAN_POINT('Ctrl Pts',(181.889794938368,1.84453883308438,329.171663869015));
#7082=CARTESIAN_POINT('Ctrl Pts',(181.882053852307,1.68253608769299,329.120393601099));
#7083=CARTESIAN_POINT('Ctrl Pts',(181.874312766246,1.51838722708001,329.075879679895));
#7084=CARTESIAN_POINT('Ctrl Pts',(181.866571680185,1.3526705309753,329.038279778694));
#7085=CARTESIAN_POINT('Ctrl Pts',(181.858831037032,1.18696331637532,329.000682028776));
#7086=CARTESIAN_POINT('Ctrl Pts',(181.851090393878,1.01968875205604,328.969997576298));
#7087=CARTESIAN_POINT('Ctrl Pts',(181.843349750725,0.851436510272571,328.946333224278));
#7088=CARTESIAN_POINT('Ctrl Pts',(181.835607595032,0.683151391608317,328.922664248189));
#7089=CARTESIAN_POINT('Ctrl Pts',(181.827865439339,0.513888524648997,328.906018157963));
#7090=CARTESIAN_POINT('Ctrl Pts',(181.820123283645,0.344244788922837,328.896450124084));
#7091=CARTESIAN_POINT('Ctrl Pts',(181.814891019959,0.229597035336734,328.889983904828));
#7092=CARTESIAN_POINT('Ctrl Pts',(181.809658756272,0.114775467815156,328.886749342777));
#7093=CARTESIAN_POINT('Ctrl Pts',(181.804426492585,-3.50001460560987E-5,
328.8867500001));
#7094=CARTESIAN_POINT('Ctrl Pts',(181.796700703164,-0.169560381862912,328.886750970683));
#7095=CARTESIAN_POINT('Ctrl Pts',(181.788974913744,-0.339113346876187,328.893807899507));
#7096=CARTESIAN_POINT('Ctrl Pts',(181.781249124323,-0.508097471414815,328.907901632275));
#7097=CARTESIAN_POINT('Ctrl Pts',(181.773524701802,-0.677051698117159,328.921992871482));
#7098=CARTESIAN_POINT('Ctrl Pts',(181.765800279281,-0.845436969768592,328.943118403924));
#7099=CARTESIAN_POINT('Ctrl Pts',(181.758075856761,-1.01266077447828,328.971207109352));
#7100=CARTESIAN_POINT('Ctrl Pts',(181.750351129555,-1.17989117521914,328.999296922719));
#7101=CARTESIAN_POINT('Ctrl Pts',(181.74262640235,-1.34595970453457,329.0343504093));
#7102=CARTESIAN_POINT('Ctrl Pts',(181.734901675144,-1.51028209450224,329.076244978265));
#7103=CARTESIAN_POINT('Ctrl Pts',(181.727177328386,-1.67459639149987,329.1181374839));
#7104=CARTESIAN_POINT('Ctrl Pts',(181.719452981628,-1.83716441457824,329.166870318647));
#7105=CARTESIAN_POINT('Ctrl Pts',(181.71172863487,-1.99741494345117,329.222270419431));
#7106=CARTESIAN_POINT('Ctrl Pts',(181.704002541135,-2.1577017153836,329.277683049779));
#7107=CARTESIAN_POINT('Ctrl Pts',(181.696276447399,-2.31566964619419,329.339765856229));
#7108=CARTESIAN_POINT('Ctrl Pts',(181.688550353664,-2.47076463802303,329.40829653272));
#7109=CARTESIAN_POINT('Ctrl Pts',(181.683236626639,-2.57743334770278,329.455429446223));
#7110=CARTESIAN_POINT('Ctrl Pts',(181.677922899614,-2.68274346761574,329.505611299942));
#7111=CARTESIAN_POINT('Ctrl Pts',(181.672609172588,-2.7865206371216,329.558756732015));
#7112=CARTESIAN_POINT('Ctrl Pts',(181.664863530544,-2.93779314386834,329.636225049662));
#7113=CARTESIAN_POINT('Ctrl Pts',(181.657117888501,-3.08585657722454,329.720017559832));
#7114=CARTESIAN_POINT('Ctrl Pts',(181.649372246457,-3.23018632527504,329.80984375317));
#7115=CARTESIAN_POINT('Ctrl Pts',(181.641627509334,-3.3744992113262,329.899659452142));
#7116=CARTESIAN_POINT('Ctrl Pts',(181.633882772212,-3.51507901533247,329.995507264189));
#7117=CARTESIAN_POINT('Ctrl Pts',(181.626138035089,-3.65142820285723,330.09705214775));
#7118=CARTESIAN_POINT('Ctrl Pts',(181.618394362755,-3.78775864433969,330.198583070358));
#7119=CARTESIAN_POINT('Ctrl Pts',(181.610650690422,-3.91985937979659,330.305809313032));
#7120=CARTESIAN_POINT('Ctrl Pts',(181.602907018089,-4.04726388326374,330.418353939715));
#7121=CARTESIAN_POINT('Ctrl Pts',(181.595162963828,-4.17467467047373,330.530904117233));
#7122=CARTESIAN_POINT('Ctrl Pts',(181.587418909567,-4.29738852701738,330.648772996642));
#7123=CARTESIAN_POINT('Ctrl Pts',(181.579674855307,-4.41497333122138,330.771544484436));
#7124=CARTESIAN_POINT('Ctrl Pts',(181.575287110396,-4.48159633112227,330.841106234991));
#7125=CARTESIAN_POINT('Ctrl Pts',(181.570899365485,-4.54657339642634,330.912241177313));
#7126=CARTESIAN_POINT('Ctrl Pts',(181.566511620574,-4.60983126052084,330.984868456448));
#7127=CARTESIAN_POINT('Ctrl Pts',(182.104574390455,-4.16808369392609,331.997787668581));
#7128=CARTESIAN_POINT('Ctrl Pts',(182.024840110229,-4.22040928104604,331.815253763263));
#7129=CARTESIAN_POINT('Ctrl Pts',(181.939623298558,-4.28217880461786,331.639873365627));
#7130=CARTESIAN_POINT('Ctrl Pts',(181.758511384681,-4.42957189444357,331.300341201909));
#7131=CARTESIAN_POINT('Ctrl Pts',(181.66421667762,-4.51390798575797,331.139204559319));
#7132=CARTESIAN_POINT('Ctrl Pts',(181.566513177962,-4.60957431560398,330.985046921468));
#7133=CARTESIAN_POINT('Ctrl Pts',(185.231676812499,-1.57888188187688,329.094159029776));
#7134=CARTESIAN_POINT('Ctrl Pts',(185.231676812499,-1.73835198187131,329.150566371651));
#7135=CARTESIAN_POINT('Ctrl Pts',(185.231676812499,-1.89508205965106,329.213606388089));
#7136=CARTESIAN_POINT('Ctrl Pts',(185.231676812499,-2.04872667936675,329.282990086686));
#7137=CARTESIAN_POINT('Ctrl Pts',(185.231676812499,-2.20308815783609,329.352697508377));
#7138=CARTESIAN_POINT('Ctrl Pts',(185.231676812499,-2.35433594020408,329.42880840094));
#7139=CARTESIAN_POINT('Ctrl Pts',(185.231676812499,-2.5020949046273,329.511076494482));
#7140=CARTESIAN_POINT('Ctrl Pts',(185.231676812499,-2.64871564282186,329.592710855226));
#7141=CARTESIAN_POINT('Ctrl Pts',(185.231676812499,-2.79190164442619,329.680408433974));
#7142=CARTESIAN_POINT('Ctrl Pts',(185.231676812499,-2.93125343180188,329.773967200279));
#7143=CARTESIAN_POINT('Ctrl Pts',(185.231676812499,-3.06871479501524,329.866256763256));
#7144=CARTESIAN_POINT('Ctrl Pts',(185.231676812499,-3.20244572065316,329.964250061903));
#7145=CARTESIAN_POINT('Ctrl Pts',(185.231676812499,-3.33202330707788,330.067783390882));
#7146=CARTESIAN_POINT('Ctrl Pts',(185.231676812499,-3.38627701191309,330.111132451673));
#7147=CARTESIAN_POINT('Ctrl Pts',(185.231676812499,-3.43980208895837,330.155453043346));
#7148=CARTESIAN_POINT('Ctrl Pts',(185.231676812499,-3.4925651108654,330.200734444903));
#7149=CARTESIAN_POINT('Ctrl Pts',(185.231676812499,-3.5182625935215,330.222788110313));
#7150=CARTESIAN_POINT('Ctrl Pts',(185.231676812499,-3.54377929119041,330.245069694118));
#7151=CARTESIAN_POINT('Ctrl Pts',(185.231676812499,-3.56911120994015,330.26757801486));
#7152=CARTESIAN_POINT('Ctrl Pts',(185.231676812499,-3.58437253362646,330.281138249751));
#7153=CARTESIAN_POINT('Ctrl Pts',(185.231676812499,-3.59956441158646,330.294778713852));
#7154=CARTESIAN_POINT('Ctrl Pts',(185.231676812499,-3.61467856278962,330.308492172096));
#7155=CARTESIAN_POINT('Ctrl Pts',(185.231676812499,-3.72900933401943,330.41222742234));
#7156=CARTESIAN_POINT('Ctrl Pts',(185.231676812499,-3.83902172849591,330.520249660355));
#7157=CARTESIAN_POINT('Ctrl Pts',(185.231676812499,-3.94442751503383,330.632378002573));
#7158=CARTESIAN_POINT('Ctrl Pts',(185.231676812499,-4.05752303973181,330.752686518009));
#7159=CARTESIAN_POINT('Ctrl Pts',(185.231676812499,-4.16531615956235,330.877722271505));
#7160=CARTESIAN_POINT('Ctrl Pts',(185.231676812499,-4.26759160960737,331.007088100841));
#7161=CARTESIAN_POINT('Ctrl Pts',(185.231676812499,-4.36956160869967,331.136067572397));
#7162=CARTESIAN_POINT('Ctrl Pts',(185.231676812499,-4.46604714172357,331.269352010455));
#7163=CARTESIAN_POINT('Ctrl Pts',(185.231676812499,-4.55678877768288,331.406570494987));
#7164=CARTESIAN_POINT('Ctrl Pts',(185.231676812499,-4.63744662151081,331.528540382115));
#7165=CARTESIAN_POINT('Ctrl Pts',(185.231676812499,-4.71356574636673,331.653619176505));
#7166=CARTESIAN_POINT('Ctrl Pts',(185.231676812499,-4.78493037128097,331.78155472816));
#7167=CARTESIAN_POINT('Ctrl Pts',(185.231676812499,-4.81541526497096,331.83620507763));
#7168=CARTESIAN_POINT('Ctrl Pts',(185.231676812499,-4.8450321714567,331.891376775287));
#7169=CARTESIAN_POINT('Ctrl Pts',(185.231676812499,-4.87376238450164,331.947050328813));
#7170=CARTESIAN_POINT('Ctrl Pts',(185.231676812499,-4.88925064968163,331.977063568157));
#7171=CARTESIAN_POINT('Ctrl Pts',(185.231676812499,-4.90448120272001,332.007222658275));
#7172=CARTESIAN_POINT('Ctrl Pts',(185.231676812499,-4.91945097087971,332.037524544675));
#7173=CARTESIAN_POINT('Ctrl Pts',(185.231676812499,-4.9311703709993,332.061247018351));
#7174=CARTESIAN_POINT('Ctrl Pts',(185.231676812499,-4.94273150315958,332.085060457977));
#7175=CARTESIAN_POINT('Ctrl Pts',(185.231676812499,-4.95412148534072,332.108939074973));
#7176=CARTESIAN_POINT('Ctrl Pts',(185.231676812499,-5.02353469935308,332.254460948973));
#7177=CARTESIAN_POINT('Ctrl Pts',(185.231676812499,-5.08668092357429,332.402570634041));
#7178=CARTESIAN_POINT('Ctrl Pts',(185.231676812499,-5.14335414057236,332.55290189119));
#7179=CARTESIAN_POINT('Ctrl Pts',(185.231676812499,-5.19772593705412,332.697128405079));
#7180=CARTESIAN_POINT('Ctrl Pts',(185.231676812499,-5.24613970701393,332.843400400837));
#7181=CARTESIAN_POINT('Ctrl Pts',(185.231676812499,-5.2883700108282,332.991406338361));
#7182=CARTESIAN_POINT('Ctrl Pts',(185.231676812499,-5.33253917815909,333.14620747475));
#7183=CARTESIAN_POINT('Ctrl Pts',(185.231676812499,-5.36994432102688,333.302906181851));
#7184=CARTESIAN_POINT('Ctrl Pts',(185.231676812499,-5.4005338396348,333.46105196999));
#7185=CARTESIAN_POINT('Ctrl Pts',(185.231676812499,-5.43080057094012,333.617528969122));
#7186=CARTESIAN_POINT('Ctrl Pts',(185.231676812499,-5.45439463767241,333.775423415486));
#7187=CARTESIAN_POINT('Ctrl Pts',(185.231676812499,-5.47121620981323,333.934290241842));
#7188=CARTESIAN_POINT('Ctrl Pts',(185.231676812499,-5.47970963242515,334.014504093672));
#7189=CARTESIAN_POINT('Ctrl Pts',(185.231676812499,-5.48647571610912,334.094965633454));
#7190=CARTESIAN_POINT('Ctrl Pts',(185.231676812499,-5.49149684516094,334.175615808331));
#7191=CARTESIAN_POINT('Ctrl Pts',(185.231676812499,-5.49271232726811,334.195139075606));
#7192=CARTESIAN_POINT('Ctrl Pts',(185.231676812499,-5.49382492256659,334.214663472413));
#7193=CARTESIAN_POINT('Ctrl Pts',(185.231676812499,-5.49483465321806,334.234187817882));
#7194=CARTESIAN_POINT('Ctrl Pts',(185.231676812499,-5.5029708203841,334.391510306122));
#7195=CARTESIAN_POINT('Ctrl Pts',(185.231676812499,-5.50443303249865,334.548837541304));
#7196=CARTESIAN_POINT('Ctrl Pts',(185.231676812499,-5.4992155195584,334.705746654721));
#7197=CARTESIAN_POINT('Ctrl Pts',(185.231676812499,-5.49404352625385,334.861286831297));
#7198=CARTESIAN_POINT('Ctrl Pts',(185.231676812499,-5.48230771340722,335.016416879734));
#7199=CARTESIAN_POINT('Ctrl Pts',(185.231676812499,-5.46395236187144,335.170717561847));
#7200=CARTESIAN_POINT('Ctrl Pts',(185.231676812499,-5.44693143715193,335.313800645235));
#7201=CARTESIAN_POINT('Ctrl Pts',(185.231676812499,-5.42421792833861,335.456170938082));
#7202=CARTESIAN_POINT('Ctrl Pts',(185.231676812499,-5.39572976443111,335.597480368818));
#7203=CARTESIAN_POINT('Ctrl Pts',(185.231676812499,-5.36488434807988,335.750482445033));
#7204=CARTESIAN_POINT('Ctrl Pts',(185.231676812499,-5.32726895980449,335.902241751547));
#7205=CARTESIAN_POINT('Ctrl Pts',(185.231676812499,-5.28300576036397,336.052318876615));
#7206=CARTESIAN_POINT('Ctrl Pts',(185.231676812499,-5.26896492839455,336.099925188905));
#7207=CARTESIAN_POINT('Ctrl Pts',(185.231676812499,-5.25425487034703,336.14736198236));
#7208=CARTESIAN_POINT('Ctrl Pts',(185.231676812499,-5.2388786826432,336.194614475456));
#7209=CARTESIAN_POINT('Ctrl Pts',(185.231676812499,-5.23167458064542,336.216753368819));
#7210=CARTESIAN_POINT('Ctrl Pts',(185.231676812499,-5.22432424857934,336.238851799957));
#7211=CARTESIAN_POINT('Ctrl Pts',(185.231676812499,-5.21682797777118,336.260908217447));
#7212=CARTESIAN_POINT('Ctrl Pts',(185.231676812499,-5.2096173598859,336.282124153012));
#7213=CARTESIAN_POINT('Ctrl Pts',(185.231676812499,-5.20227473994666,336.303292285562));
#7214=CARTESIAN_POINT('Ctrl Pts',(185.231676812499,-5.1948013758209,336.324409488964));
#7215=CARTESIAN_POINT('Ctrl Pts',(185.231676812499,-5.14337557704968,336.469721430745));
#7216=CARTESIAN_POINT('Ctrl Pts',(185.231676812499,-5.08575233256317,336.612653986095));
#7217=CARTESIAN_POINT('Ctrl Pts',(185.231676812499,-5.02210170694438,336.752803828727));
#7218=CARTESIAN_POINT('Ctrl Pts',(185.231676812499,-4.95893748112331,336.891882686519));
#7219=CARTESIAN_POINT('Ctrl Pts',(185.231676812499,-4.88983719424972,337.028221804996));
#7220=CARTESIAN_POINT('Ctrl Pts',(185.231676812499,-4.81492740369595,337.161395345287));
#7221=CARTESIAN_POINT('Ctrl Pts',(185.231676812499,-4.77883982411297,337.225551321403));
#7222=CARTESIAN_POINT('Ctrl Pts',(185.231676812499,-4.74140342345992,337.288972099951));
#7223=CARTESIAN_POINT('Ctrl Pts',(185.231676812499,-4.70262948771864,337.351606785902));
#7224=CARTESIAN_POINT('Ctrl Pts',(185.231676812499,-4.68910049919007,337.373461259313));
#7225=CARTESIAN_POINT('Ctrl Pts',(185.231676812499,-4.675407234967,337.395222225542));
#7226=CARTESIAN_POINT('Ctrl Pts',(185.231676812499,-4.66155480165754,337.416880163837));
#7227=CARTESIAN_POINT('Ctrl Pts',(185.231676812499,-4.58035938880544,337.543827191992));
#7228=CARTESIAN_POINT('Ctrl Pts',(185.231676812499,-4.4937984836642,337.667083797264));
#7229=CARTESIAN_POINT('Ctrl Pts',(185.231676812499,-4.40201176383362,337.786251222207));
#7230=CARTESIAN_POINT('Ctrl Pts',(185.231676812499,-4.38153716639785,337.812833554136));
#7231=CARTESIAN_POINT('Ctrl Pts',(185.231676812499,-4.36080239410286,337.839212266764));
#7232=CARTESIAN_POINT('Ctrl Pts',(185.231676812499,-4.33980875715192,337.86538267042));
#7233=CARTESIAN_POINT('Ctrl Pts',(185.231676812499,-4.24507766023181,337.983473263819));
#7234=CARTESIAN_POINT('Ctrl Pts',(185.231676812499,-4.1450777393752,338.097325920217));
#7235=CARTESIAN_POINT('Ctrl Pts',(185.231676812499,-4.04013750288101,338.206631798415));
#7236=CARTESIAN_POINT('Ctrl Pts',(185.231676812499,-3.98795564423823,338.260984485958));
#7237=CARTESIAN_POINT('Ctrl Pts',(185.231676812499,-3.93455183338055,338.314212240782));
#7238=CARTESIAN_POINT('Ctrl Pts',(185.231676812499,-3.87996446941807,338.366272709916));
#7239=CARTESIAN_POINT('Origin',(189.09641784506,0.,335.));
#7240=CARTESIAN_POINT('',(181.433471471437,-4.42539066683714,330.782448221021));
#7241=CARTESIAN_POINT('Ctrl Pts',(181.56641430909,-4.60985083416171,330.984890929342));
#7242=CARTESIAN_POINT('Ctrl Pts',(181.522338792745,-4.54928340234734,330.915351890387));
#7243=CARTESIAN_POINT('Ctrl Pts',(181.477947892443,-4.48772044764387,330.847849582925));
#7244=CARTESIAN_POINT('Ctrl Pts',(181.433471471437,-4.4253906668373,330.782448221021));
#7245=CARTESIAN_POINT('',(181.93402621666,5.10326494491037,331.634214435745));
#7246=CARTESIAN_POINT('Ctrl Pts',(181.93402621666,5.10326494491053,331.634214435745));
#7247=CARTESIAN_POINT('Ctrl Pts',(181.990740853293,5.17775085053129,331.747151312973));
#7248=CARTESIAN_POINT('Ctrl Pts',(182.045657125741,5.2491901014954,331.863643016254));
#7249=CARTESIAN_POINT('Ctrl Pts',(182.09819904041,5.31704363992713,331.983234763259));
#7250=CARTESIAN_POINT('Ctrl Pts',(181.93402621666,5.10326494491048,331.634214435745));
#7251=CARTESIAN_POINT('Ctrl Pts',(181.926218208781,5.00890916558778,331.491150496651));
#7252=CARTESIAN_POINT('Ctrl Pts',(181.918410200902,4.90853007055727,331.352050989582));
#7253=CARTESIAN_POINT('Ctrl Pts',(181.910602193022,4.8024832581551,331.217410924031));
#7254=CARTESIAN_POINT('Ctrl Pts',(181.902794646657,4.69644271394199,331.082778816752));
#7255=CARTESIAN_POINT('Ctrl Pts',(181.894987100292,4.58473530854143,330.952605861636));
#7256=CARTESIAN_POINT('Ctrl Pts',(181.887179553927,4.4677576066271,330.827354852024));
#7257=CARTESIAN_POINT('Ctrl Pts',(181.879371329259,4.35076974194103,330.702092960874));
#7258=CARTESIAN_POINT('Ctrl Pts',(181.87156310459,4.22851087061426,330.581754091798));
#7259=CARTESIAN_POINT('Ctrl Pts',(181.863754879922,4.10141575942253,330.466765577332));
#7260=CARTESIAN_POINT('Ctrl Pts',(181.855946921021,3.97432497414003,330.351780976706));
#7261=CARTESIAN_POINT('Ctrl Pts',(181.84813896212,3.84239850333922,330.242146567915));
#7262=CARTESIAN_POINT('Ctrl Pts',(181.840331003219,3.70610593010505,330.138250891157));
#7263=CARTESIAN_POINT('Ctrl Pts',(181.832522197085,3.56979856793164,330.034343940806));
#7264=CARTESIAN_POINT('Ctrl Pts',(181.824713390952,3.42912439710866,329.936177149669));
#7265=CARTESIAN_POINT('Ctrl Pts',(181.816904584819,3.28458452298962,329.844097550008));
#7266=CARTESIAN_POINT('Ctrl Pts',(181.814232233331,3.23511968276336,329.81258581172));
#7267=CARTESIAN_POINT('Ctrl Pts',(181.811559881842,3.18520235873944,329.781786612718));
#7268=CARTESIAN_POINT('Ctrl Pts',(181.808887530354,3.13485339884983,329.751712686007));
#7269=CARTESIAN_POINT('Ctrl Pts',(181.801150672344,2.98908561519292,329.66464416161));
#7270=CARTESIAN_POINT('Ctrl Pts',(181.793413814334,2.83967110941098,329.583642068593));
#7271=CARTESIAN_POINT('Ctrl Pts',(181.785676956324,2.68713419412161,329.508995047782));
#7272=CARTESIAN_POINT('Ctrl Pts',(181.777941031189,2.53461567104635,329.434357027573));
#7273=CARTESIAN_POINT('Ctrl Pts',(181.770205106055,2.37897577251338,329.366072688317));
#7274=CARTESIAN_POINT('Ctrl Pts',(181.76246918092,2.22076193399246,329.30438396703));
#7275=CARTESIAN_POINT('Ctrl Pts',(181.754732579435,2.06253426287033,329.242689852311));
#7276=CARTESIAN_POINT('Ctrl Pts',(181.746995977951,1.90173249432713,329.18759262466));
#7277=CARTESIAN_POINT('Ctrl Pts',(181.739259376466,1.73892322056481,329.139285743574));
#7278=CARTESIAN_POINT('Ctrl Pts',(181.731522841827,1.57611535350781,329.090979279868));
#7279=CARTESIAN_POINT('Ctrl Pts',(181.723786307188,1.4113003184333,329.049463132175));
#7280=CARTESIAN_POINT('Ctrl Pts',(181.716049772549,1.24505923772503,329.014880698177));
#7281=CARTESIAN_POINT('Ctrl Pts',(181.708311535401,1.07878157385147,328.980290653937));
#7282=CARTESIAN_POINT('Ctrl Pts',(181.700573298253,0.911077545689822,328.952637435205));
#7283=CARTESIAN_POINT('Ctrl Pts',(181.692835061105,0.742538621281503,328.932013352157));
#7284=CARTESIAN_POINT('Ctrl Pts',(181.689806322086,0.676572638743626,328.92394110471));
#7285=CARTESIAN_POINT('Ctrl Pts',(181.686777583067,0.610478838334116,328.91694511559));
#7286=CARTESIAN_POINT('Ctrl Pts',(181.683748844048,0.544292940753909,328.911028760361));
#7287=CARTESIAN_POINT('Ctrl Pts',(181.676010618166,0.375192393463351,328.895912867948));
#7288=CARTESIAN_POINT('Ctrl Pts',(181.668272392283,0.205433266660727,328.887843045992));
#7289=CARTESIAN_POINT('Ctrl Pts',(181.660534166401,0.0356130198117278,328.886853733525));
#7290=CARTESIAN_POINT('Ctrl Pts',(181.652797465714,-0.134173755661763,328.88586461605));
#7291=CARTESIAN_POINT('Ctrl Pts',(181.645060765027,-0.3040213126236,328.891953225026));
#7292=CARTESIAN_POINT('Ctrl Pts',(181.63732406434,-0.473331423985043,328.90510189375));
#7293=CARTESIAN_POINT('Ctrl Pts',(181.62958756594,-0.64263710848922,328.918250218683));
#7294=CARTESIAN_POINT('Ctrl Pts',(181.62185106754,-0.811405061496992,328.938458213732));
#7295=CARTESIAN_POINT('Ctrl Pts',(181.61411456914,-0.979040697736622,328.965656218388));
#7296=CARTESIAN_POINT('Ctrl Pts',(181.606378644741,-1.14666389644456,328.99285220512));
#7297=CARTESIAN_POINT('Ctrl Pts',(181.598642720342,-1.31315463580628,329.027037113852));
#7298=CARTESIAN_POINT('Ctrl Pts',(181.590906795942,-1.47792674418541,329.068089843792));
#7299=CARTESIAN_POINT('Ctrl Pts',(181.583169911958,-1.64271929133618,329.109147666022));
#7300=CARTESIAN_POINT('Ctrl Pts',(181.575433027974,-1.80579247617785,329.157074935507));
#7301=CARTESIAN_POINT('Ctrl Pts',(181.56769614399,-1.96657281252487,329.211699996066));
#7302=CARTESIAN_POINT('Ctrl Pts',(181.564667481908,-2.02951149808858,329.233083391502));
#7303=CARTESIAN_POINT('Ctrl Pts',(181.561638819825,-2.09209899386936,329.25549261054));
#7304=CARTESIAN_POINT('Ctrl Pts',(181.558610157743,-2.15430159130236,329.278915293739));
#7305=CARTESIAN_POINT('Ctrl Pts',(181.550801355749,-2.31467860055276,329.339306017522));
#7306=CARTESIAN_POINT('Ctrl Pts',(181.542992553756,-2.47252542602931,329.40644852171));
#7307=CARTESIAN_POINT('Ctrl Pts',(181.535183751763,-2.62728026094965,329.480106523408));
#7308=CARTESIAN_POINT('Ctrl Pts',(181.527375758222,-2.78201907395733,329.553756899224));
#7309=CARTESIAN_POINT('Ctrl Pts',(181.519567764681,-2.93366626292296,329.633921295823));
#7310=CARTESIAN_POINT('Ctrl Pts',(181.51175977114,-3.08168227924436,329.720316307553));
#7311=CARTESIAN_POINT('Ctrl Pts',(181.503951611735,-3.22970143984743,329.806713154559));
#7312=CARTESIAN_POINT('Ctrl Pts',(181.496143452331,-3.37408901161883,329.899340730889));
#7313=CARTESIAN_POINT('Ctrl Pts',(181.488335292926,-3.51433151700546,329.997870498369));
#7314=CARTESIAN_POINT('Ctrl Pts',(181.480527696507,-3.65456391059011,330.096393161631));
#7315=CARTESIAN_POINT('Ctrl Pts',(181.472720100088,-3.79065158843474,330.200816991173));
#7316=CARTESIAN_POINT('Ctrl Pts',(181.464912503669,-3.92211110399618,330.310770846886));
#7317=CARTESIAN_POINT('Ctrl Pts',(181.45710449039,-4.05357763839256,330.420730573213));
#7318=CARTESIAN_POINT('Ctrl Pts',(181.449296477111,-4.18041528485859,330.53622072209));
#7319=CARTESIAN_POINT('Ctrl Pts',(181.441488463832,-4.30217403518314,330.656830174458));
#7320=CARTESIAN_POINT('Ctrl Pts',(181.438816133034,-4.34384656401224,330.698109350431));
#7321=CARTESIAN_POINT('Ctrl Pts',(181.436143802235,-4.38492446347651,330.73998786296));
#7322=CARTESIAN_POINT('Ctrl Pts',(181.433471471437,-4.42539066683728,330.782448221021));
#7323=CARTESIAN_POINT('Origin',(189.09641784506,0.,335.));
#7324=CARTESIAN_POINT('',(180.763832419144,3.42440815596402,340.064114369154));
#7325=CARTESIAN_POINT('Origin',(181.305293072034,1.78859679747709,337.316743696534));
#7326=CARTESIAN_POINT('',(181.127182464992,-3.98471776201124,339.636029163189));
#7327=CARTESIAN_POINT('Ctrl Pts',(181.127182464992,-3.98471776201124,339.636029163189));
#7328=CARTESIAN_POINT('Ctrl Pts',(181.067955450267,-2.99815593998204,340.482329942323));
#7329=CARTESIAN_POINT('Ctrl Pts',(180.946838768317,-0.4141468295078,341.549221172133));
#7330=CARTESIAN_POINT('Ctrl Pts',(180.825722086368,2.29912071323036,340.825045741512));
#7331=CARTESIAN_POINT('Ctrl Pts',(180.763832419144,3.42440815596409,340.064114369154));
#7332=CARTESIAN_POINT('',(180.967537046477,-3.74458518213069,339.832174187285));
#7333=CARTESIAN_POINT('Ctrl Pts',(180.967537046477,-3.74458518213077,339.832174187285));
#7334=CARTESIAN_POINT('Ctrl Pts',(181.021129560953,-3.82667683118351,339.768559102086));
#7335=CARTESIAN_POINT('Ctrl Pts',(181.074441913781,-3.9067932259694,339.703123245957));
#7336=CARTESIAN_POINT('Ctrl Pts',(181.127155953893,-3.98478354106129,339.636089482893));
#7337=CARTESIAN_POINT('Ctrl Pts',(180.967537046477,-3.74458518213076,339.832174187285));
#7338=CARTESIAN_POINT('Ctrl Pts',(180.928811024139,-3.07271202188714,340.352827247918));
#7339=CARTESIAN_POINT('Ctrl Pts',(180.838450305348,-1.24788233890097,341.236855210088));
#7340=CARTESIAN_POINT('Ctrl Pts',(180.748089586558,0.810419303791811,341.164371694386));
#7341=CARTESIAN_POINT('Ctrl Pts',(180.696454890107,1.88832481980924,340.814297458627));
#7342=CARTESIAN_POINT('Ctrl Pts',(185.231361012054,3.8792849430986,338.366214240201));
#7343=CARTESIAN_POINT('Ctrl Pts',(185.185572085065,4.43269208993578,337.728459763145));
#7344=CARTESIAN_POINT('Ctrl Pts',(185.094000440801,5.21810240427798,336.175231791177));
#7345=CARTESIAN_POINT('Ctrl Pts',(184.956646079264,5.15285959308729,333.5646422366));
#7346=CARTESIAN_POINT('Ctrl Pts',(184.81929792744,3.85951183190938,331.296424465933));
#7347=CARTESIAN_POINT('Ctrl Pts',(184.681949775617,1.64650067071449,329.910579844264));
#7348=CARTESIAN_POINT('Ctrl Pts',(184.544601623793,-0.958914747099921,329.737539388153));
#7349=CARTESIAN_POINT('Ctrl Pts',(184.40725347197,-3.33582893453105,330.818465109628));
#7350=CARTESIAN_POINT('Ctrl Pts',(184.269905320146,-4.91785548454191,332.895822139143));
#7351=CARTESIAN_POINT('Ctrl Pts',(184.132557168322,-5.32799673609857,335.474578828195));
#7352=CARTESIAN_POINT('Ctrl Pts',(183.995209016499,-4.46852102288055,337.9402460905));
#7353=CARTESIAN_POINT('Ctrl Pts',(183.857860864675,-2.54423183283122,339.705271838468));
#7354=CARTESIAN_POINT('Ctrl Pts',(183.720512712852,-0.013672882354056,340.349065869959));
#7355=CARTESIAN_POINT('Ctrl Pts',(183.583164561028,2.52014341764217,339.718216674611));
#7356=CARTESIAN_POINT('Ctrl Pts',(183.445816409204,4.45342772461749,337.963051390792));
#7357=CARTESIAN_POINT('Ctrl Pts',(183.308468257381,5.32549297122311,335.501812761407));
#7358=CARTESIAN_POINT('Ctrl Pts',(183.171120105557,4.928532499482,332.920995423183));
#7359=CARTESIAN_POINT('Ctrl Pts',(183.033771953734,3.3571385152569,330.83558891529));
#7360=CARTESIAN_POINT('Ctrl Pts',(182.89642380191,0.98576231142187,329.742529137502));
#7361=CARTESIAN_POINT('Ctrl Pts',(182.759075650087,-1.62051696004763,329.902284917117));
#7362=CARTESIAN_POINT('Ctrl Pts',(182.621727498263,-3.8406417937291,331.276783964202));
#7363=CARTESIAN_POINT('Ctrl Pts',(182.48437934644,-5.14558092249528,333.53849882316));
#7364=CARTESIAN_POINT('Ctrl Pts',(182.347031194616,-5.22436997067687,336.148463143921));
#7365=CARTESIAN_POINT('Ctrl Pts',(182.209683042792,-4.0582669213237,338.484771380675));
#7366=CARTESIAN_POINT('Ctrl Pts',(182.072334890969,-1.92509982860368,339.990620599394));
#7367=CARTESIAN_POINT('Ctrl Pts',(181.934986739145,0.666666827042015,340.307331649402));
#7368=CARTESIAN_POINT('Ctrl Pts',(181.797638587322,3.09968853668966,339.359057841091));
#7369=CARTESIAN_POINT('Ctrl Pts',(181.706073152773,4.22888407421017,338.034729998404));
#7370=CARTESIAN_POINT('Ctrl Pts',(181.660290435498,4.60334381111095,337.278042084719));
#7371=CARTESIAN_POINT('Ctrl Pts',(185.419486611316,4.12539012104192,338.579769770854));
#7372=CARTESIAN_POINT('Ctrl Pts',(185.373697684327,4.71390589391333,337.901555600488));
#7373=CARTESIAN_POINT('Ctrl Pts',(185.282126040064,5.54914331505611,336.249789508214));
#7374=CARTESIAN_POINT('Ctrl Pts',(185.144771678526,5.47976144373112,333.473581903844));
#7375=CARTESIAN_POINT('Ctrl Pts',(185.007423526703,4.10436258664865,331.061466444233));
#7376=CARTESIAN_POINT('Ctrl Pts',(184.870075374879,1.75095609136382,329.587702646164));
#7377=CARTESIAN_POINT('Ctrl Pts',(184.732727223055,-1.01974912455067,329.403684354482));
#7378=CARTESIAN_POINT('Ctrl Pts',(184.595379071232,-3.54745679522268,330.553184934708));
#7379=CARTESIAN_POINT('Ctrl Pts',(184.458030919408,-5.22984847213511,332.762331283362));
#7380=CARTESIAN_POINT('Ctrl Pts',(184.320682767585,-5.66600943793726,335.504686517802));
#7381=CARTESIAN_POINT('Ctrl Pts',(184.183334615761,-4.75200784522287,338.126777834859));
#7382=CARTESIAN_POINT('Ctrl Pts',(184.045986463938,-2.70564009160373,340.003778336461));
#7383=CARTESIAN_POINT('Ctrl Pts',(183.908638312114,-0.0145403017867841,
340.688415215796));
#7384=CARTESIAN_POINT('Ctrl Pts',(183.77129016029,2.68002348660821,340.017544404157));
#7385=CARTESIAN_POINT('Ctrl Pts',(183.633942008467,4.73595701511844,338.151029923043));
#7386=CARTESIAN_POINT('Ctrl Pts',(183.496593856643,5.66334683206167,335.533648195191));
#7387=CARTESIAN_POINT('Ctrl Pts',(183.35924570482,5.24120284609892,332.789101582224));
#7388=CARTESIAN_POINT('Ctrl Pts',(183.221897552996,3.57011827410332,330.571395089348));
#7389=CARTESIAN_POINT('Ctrl Pts',(183.084549401172,1.0482999214765,329.408990657828));
#7390=CARTESIAN_POINT('Ctrl Pts',(182.947201249349,-1.72332395171299,329.578881481696));
#7391=CARTESIAN_POINT('Ctrl Pts',(182.809853097525,-4.08429541699382,331.040579932157));
#7392=CARTESIAN_POINT('Ctrl Pts',(182.672504945702,-5.47202100800777,333.445779929738));
#7393=CARTESIAN_POINT('Ctrl Pts',(182.535156793878,-5.55580850126549,336.221322634921));
#7394=CARTESIAN_POINT('Ctrl Pts',(182.397808642055,-4.31572687011933,338.705848278432));
#7395=CARTESIAN_POINT('Ctrl Pts',(182.260460490231,-2.04722981978158,340.307229868545));
#7396=CARTESIAN_POINT('Ctrl Pts',(182.123112338408,0.708960744736812,340.644033340343));
#7397=CARTESIAN_POINT('Ctrl Pts',(181.985764186584,3.29633544715907,339.635600224901));
#7398=CARTESIAN_POINT('Ctrl Pts',(181.894198752035,4.49716812213418,338.227255883257));
#7399=CARTESIAN_POINT('Ctrl Pts',(181.84841603476,4.89538390725887,337.422563036606));
#7400=CARTESIAN_POINT('Ctrl Pts',(185.607612210577,4.37149529898523,338.793325301507));
#7401=CARTESIAN_POINT('Ctrl Pts',(185.561823283589,4.99511969789087,338.074651437831));
#7402=CARTESIAN_POINT('Ctrl Pts',(185.470251639326,5.88018422583424,336.32434722525));
#7403=CARTESIAN_POINT('Ctrl Pts',(185.332897277787,5.80666329437495,333.382521571088));
#7404=CARTESIAN_POINT('Ctrl Pts',(185.195549125964,4.34921334138792,330.826508422535));
#7405=CARTESIAN_POINT('Ctrl Pts',(185.05820097414,1.85541151201316,329.264825448066));
#7406=CARTESIAN_POINT('Ctrl Pts',(184.920852822317,-1.08058350200144,329.06982932081));
#7407=CARTESIAN_POINT('Ctrl Pts',(184.783504670493,-3.75908465591431,330.287904759788));
#7408=CARTESIAN_POINT('Ctrl Pts',(184.646156518669,-5.54184145972833,332.628840427582));
#7409=CARTESIAN_POINT('Ctrl Pts',(184.508808366846,-6.00402213977596,335.534794207408));
#7410=CARTESIAN_POINT('Ctrl Pts',(184.371460215022,-5.0354946675652,338.313309579218));
#7411=CARTESIAN_POINT('Ctrl Pts',(184.234112063199,-2.86704835037625,340.302284834453));
#7412=CARTESIAN_POINT('Ctrl Pts',(184.096763911375,-0.015407721219518,341.027764561634));
#7413=CARTESIAN_POINT('Ctrl Pts',(183.959415759552,2.83990355557424,340.316872133703));
#7414=CARTESIAN_POINT('Ctrl Pts',(183.822067607728,5.0184863056194,338.339008455293));
#7415=CARTESIAN_POINT('Ctrl Pts',(183.684719455904,6.00120069290021,335.565483628977));
#7416=CARTESIAN_POINT('Ctrl Pts',(183.547371304081,5.55387319271584,332.657207741263));
#7417=CARTESIAN_POINT('Ctrl Pts',(183.410023152257,3.78309803294972,330.307201263408));
#7418=CARTESIAN_POINT('Ctrl Pts',(183.272675000434,1.11083753153113,329.075452178153));
#7419=CARTESIAN_POINT('Ctrl Pts',(183.13532684861,-1.82613094337834,329.255478046274));
#7420=CARTESIAN_POINT('Ctrl Pts',(182.997978696786,-4.32794904025854,330.804375900113));
#7421=CARTESIAN_POINT('Ctrl Pts',(182.860630544963,-5.79846109352026,333.353061036317));
#7422=CARTESIAN_POINT('Ctrl Pts',(182.723282393139,-5.88724703185409,336.29418212592));
#7423=CARTESIAN_POINT('Ctrl Pts',(182.585934241316,-4.57318681891496,338.926925176187));
#7424=CARTESIAN_POINT('Ctrl Pts',(182.448586089492,-2.16935981095946,340.623839137696));
#7425=CARTESIAN_POINT('Ctrl Pts',(182.311237937669,0.751254662431609,340.980735031283));
#7426=CARTESIAN_POINT('Ctrl Pts',(182.173889785845,3.49298235762849,339.912142608713));
#7427=CARTESIAN_POINT('Ctrl Pts',(182.082324351296,4.76545217005818,338.419781768109));
#7428=CARTESIAN_POINT('Ctrl Pts',(182.036541634022,5.18742400340681,337.567083988495));
#7429=CARTESIAN_POINT('Ctrl Pts',(185.79573780984,4.61760047692855,339.006880832161));
#7430=CARTESIAN_POINT('Ctrl Pts',(185.74994888285,5.27633350186842,338.247747275175));
#7431=CARTESIAN_POINT('Ctrl Pts',(185.658377238587,6.21122513661239,336.398904942287));
#7432=CARTESIAN_POINT('Ctrl Pts',(185.52102287705,6.13356514501877,333.291461238332));
#7433=CARTESIAN_POINT('Ctrl Pts',(185.383674725226,4.59406409612719,330.591550400835));
#7434=CARTESIAN_POINT('Ctrl Pts',(185.246326573402,1.95986693266248,328.941948249966));
#7435=CARTESIAN_POINT('Ctrl Pts',(185.108978421579,-1.14141787945219,328.735974287139));
#7436=CARTESIAN_POINT('Ctrl Pts',(184.971630269755,-3.97071251660595,330.022624584868));
#7437=CARTESIAN_POINT('Ctrl Pts',(184.834282117932,-5.85383444732154,332.495349571801));
#7438=CARTESIAN_POINT('Ctrl Pts',(184.696933966108,-6.34203484161467,335.564901897015));
#7439=CARTESIAN_POINT('Ctrl Pts',(184.559585814284,-5.31898148990753,338.499841323576));
#7440=CARTESIAN_POINT('Ctrl Pts',(184.422237662461,-3.02845660914876,340.600791332446));
#7441=CARTESIAN_POINT('Ctrl Pts',(184.284889510637,-0.0162751406522468,
341.367113907471));
#7442=CARTESIAN_POINT('Ctrl Pts',(184.147541358814,2.99978362454027,340.616199863249));
#7443=CARTESIAN_POINT('Ctrl Pts',(184.01019320699,5.30101559612035,338.526986987545));
#7444=CARTESIAN_POINT('Ctrl Pts',(183.872845055167,6.33905455373877,335.597319062762));
#7445=CARTESIAN_POINT('Ctrl Pts',(183.735496903343,5.86654353933276,332.525313900304));
#7446=CARTESIAN_POINT('Ctrl Pts',(183.598148751519,3.99607779179613,330.043007437467));
#7447=CARTESIAN_POINT('Ctrl Pts',(183.460800599696,1.17337514158575,328.741913698478));
#7448=CARTESIAN_POINT('Ctrl Pts',(183.323452447872,-1.92893793504369,328.932074610852));
#7449=CARTESIAN_POINT('Ctrl Pts',(183.186104296049,-4.57160266352325,330.568171868067));
#7450=CARTESIAN_POINT('Ctrl Pts',(183.048756144225,-6.12490117903275,333.260342142895));
#7451=CARTESIAN_POINT('Ctrl Pts',(182.911407992402,-6.21868556244271,336.367041616919));
#7452=CARTESIAN_POINT('Ctrl Pts',(182.774059840578,-4.8306467677106,339.148002073944));
#7453=CARTESIAN_POINT('Ctrl Pts',(182.636711688754,-2.29148980213735,340.940448406847));
#7454=CARTESIAN_POINT('Ctrl Pts',(182.499363536931,0.793548580126407,341.317436722223));
#7455=CARTESIAN_POINT('Ctrl Pts',(182.362015385107,3.6896292680979,340.188684992523));
#7456=CARTESIAN_POINT('Ctrl Pts',(182.270449950558,5.03373621798219,338.612307652963));
#7457=CARTESIAN_POINT('Ctrl Pts',(182.224667233284,5.47946409955473,337.711604940384));
#7458=CARTESIAN_POINT('',(181.756492029768,3.56482183513016,338.698411259755));
#7459=CARTESIAN_POINT('Ctrl Pts',(182.22440740295,5.4790607473474,337.711405334762));
#7460=CARTESIAN_POINT('Ctrl Pts',(182.142804741226,5.18929109068282,337.921859087869));
#7461=CARTESIAN_POINT('Ctrl Pts',(182.059571383508,4.87878498043077,338.108495568584));
#7462=CARTESIAN_POINT('Ctrl Pts',(181.901355642956,4.23927546969376,338.434860777857));
#7463=CARTESIAN_POINT('Ctrl Pts',(181.825122559984,3.9053528405947,338.577120586524));
#7464=CARTESIAN_POINT('Ctrl Pts',(181.756589936366,3.56482809562168,338.69804120123));
#7465=CARTESIAN_POINT('Ctrl Pts',(185.231676812499,3.87994761181598,338.366334370211));
#7466=CARTESIAN_POINT('Ctrl Pts',(185.231676812499,3.98887908888609,338.26227654353));
#7467=CARTESIAN_POINT('Ctrl Pts',(185.231676812499,4.09289145755542,338.153540045282));
#7468=CARTESIAN_POINT('Ctrl Pts',(185.231676812499,4.19185479778346,338.040592391316));
#7469=CARTESIAN_POINT('Ctrl Pts',(185.231676812499,4.29083907028961,337.927620847173));
#7470=CARTESIAN_POINT('Ctrl Pts',(185.231676812499,4.3847726230792,337.810435804385));
#7471=CARTESIAN_POINT('Ctrl Pts',(185.231676812499,4.47350176833772,337.689455228141));
#7472=CARTESIAN_POINT('Ctrl Pts',(185.231676812499,4.56329988235493,337.567017132431));
#7473=CARTESIAN_POINT('Ctrl Pts',(185.231676812499,4.64776796769129,337.440690993295));
#7474=CARTESIAN_POINT('Ctrl Pts',(185.231676812499,4.72671497984256,337.31086694092));
#7475=CARTESIAN_POINT('Ctrl Pts',(185.231676812499,4.80373291167902,337.184215155829));
#7476=CARTESIAN_POINT('Ctrl Pts',(185.231676812499,4.87549659502638,337.054233621307));
#7477=CARTESIAN_POINT('Ctrl Pts',(185.231676812499,4.94179273439114,336.921253015162));
#7478=CARTESIAN_POINT('Ctrl Pts',(185.231676812499,4.95944215239198,336.885850798286));
#7479=CARTESIAN_POINT('Ctrl Pts',(185.231676812499,4.9767038507218,336.850235880878));
#7480=CARTESIAN_POINT('Ctrl Pts',(185.231676812499,4.9935733184925,336.814414206659));
#7481=CARTESIAN_POINT('Ctrl Pts',(185.231676812499,5.00746136130366,336.784923475127));
#7482=CARTESIAN_POINT('Ctrl Pts',(185.231676812499,5.02108356015116,336.755292608717));
#7483=CARTESIAN_POINT('Ctrl Pts',(185.231676812499,5.03443728573539,336.725524870692));
#7484=CARTESIAN_POINT('Ctrl Pts',(185.231676812499,5.04217089902195,336.708285324106));
#7485=CARTESIAN_POINT('Ctrl Pts',(185.231676812499,5.04981262271537,336.691003908423));
#7486=CARTESIAN_POINT('Ctrl Pts',(185.231676812499,5.05735898264887,336.673688581363));
#7487=CARTESIAN_POINT('Ctrl Pts',(185.231676812499,5.11956259584394,336.530960707751));
#7488=CARTESIAN_POINT('Ctrl Pts',(185.231676812499,5.17535555766318,336.385785177069));
#7489=CARTESIAN_POINT('Ctrl Pts',(185.231676812499,5.22457476715685,336.238591709152));
#7490=CARTESIAN_POINT('Ctrl Pts',(185.231676812499,5.23101520818529,336.21933112249));
#7491=CARTESIAN_POINT('Ctrl Pts',(185.231676812499,5.23734304307221,336.200035929469));
#7492=CARTESIAN_POINT('Ctrl Pts',(185.231676812499,5.24355786134782,336.180707045276));
#7493=CARTESIAN_POINT('Ctrl Pts',(185.231676812499,5.29059944982507,336.03440165458));
#7494=CARTESIAN_POINT('Ctrl Pts',(185.231676812499,5.33116954348734,335.886168433814));
#7495=CARTESIAN_POINT('Ctrl Pts',(185.231676812499,5.36533293185482,335.73645063595));
#7496=CARTESIAN_POINT('Ctrl Pts',(185.231676812499,5.39984925438767,335.585186137699));
#7497=CARTESIAN_POINT('Ctrl Pts',(185.231676812499,5.42782602535396,335.432405558752));
#7498=CARTESIAN_POINT('Ctrl Pts',(185.231676812499,5.44928286384492,335.278541235197));
#7499=CARTESIAN_POINT('Ctrl Pts',(185.231676812499,5.47082747880391,335.124047477493));
#7500=CARTESIAN_POINT('Ctrl Pts',(185.231676812499,5.48579888563856,334.96846034964));
#7501=CARTESIAN_POINT('Ctrl Pts',(185.231676812499,5.49416675161173,334.812203344854));
#7502=CARTESIAN_POINT('Ctrl Pts',(185.231676812499,5.49544915618552,334.788256415222));
#7503=CARTESIAN_POINT('Ctrl Pts',(185.231676812499,5.49657636724469,334.764293738091));
#7504=CARTESIAN_POINT('Ctrl Pts',(185.231676812499,5.49754816778483,334.740316825971));
#7505=CARTESIAN_POINT('Ctrl Pts',(185.231676812499,5.4984004910039,334.719287738131));
#7506=CARTESIAN_POINT('Ctrl Pts',(185.231676812499,5.49913331564855,334.698246030343));
#7507=CARTESIAN_POINT('Ctrl Pts',(185.231676812499,5.49974632691056,334.677197959552));
#7508=CARTESIAN_POINT('Ctrl Pts',(185.231676812499,5.50439948919236,334.517429134441));
#7509=CARTESIAN_POINT('Ctrl Pts',(185.231676812499,5.50214028330716,334.357775528399));
#7510=CARTESIAN_POINT('Ctrl Pts',(185.231676812499,5.49304585829882,334.198707600937));
#7511=CARTESIAN_POINT('Ctrl Pts',(185.231676812499,5.48395143329048,334.039639673475));
#7512=CARTESIAN_POINT('Ctrl Pts',(185.231676812499,5.46802189731941,333.881156663705));
#7513=CARTESIAN_POINT('Ctrl Pts',(185.231676812499,5.44528583335869,333.723709915607));
#7514=CARTESIAN_POINT('Ctrl Pts',(185.231676812499,5.43418336044101,333.646825532287));
#7515=CARTESIAN_POINT('Ctrl Pts',(185.231676812499,5.42145708271963,333.570188034188));
#7516=CARTESIAN_POINT('Ctrl Pts',(185.231676812499,5.40710599800657,333.493849160467));
#7517=CARTESIAN_POINT('Ctrl Pts',(185.231676812499,5.37769011372305,333.337374892452));
#7518=CARTESIAN_POINT('Ctrl Pts',(185.231676812499,5.34145116456449,333.182154935493));
#7519=CARTESIAN_POINT('Ctrl Pts',(185.231676812499,5.29861321794033,333.028558091743));
#7520=CARTESIAN_POINT('Ctrl Pts',(185.231676812499,5.27225910298788,332.934064559828));
#7521=CARTESIAN_POINT('Ctrl Pts',(185.231676812499,5.24340636780778,332.840185356584));
#7522=CARTESIAN_POINT('Ctrl Pts',(185.231676812499,5.21209752347118,332.747007855073));
#7523=CARTESIAN_POINT('Ctrl Pts',(185.231676812499,5.19774869360684,332.704304646293));
#7524=CARTESIAN_POINT('Ctrl Pts',(185.231676812499,5.18288388705462,332.661748845767));
#7525=CARTESIAN_POINT('Ctrl Pts',(185.231676812499,5.16750670028485,332.619349011203));
#7526=CARTESIAN_POINT('Ctrl Pts',(185.231676812499,5.16013741342817,332.599029524404));
#7527=CARTESIAN_POINT('Ctrl Pts',(185.231676812499,5.15265044561141,332.578745859302));
#7528=CARTESIAN_POINT('Ctrl Pts',(185.231676812499,5.14504616788639,332.558498967188));
#7529=CARTESIAN_POINT('Ctrl Pts',(185.231676812499,5.13740571884857,332.538155766562));
#7530=CARTESIAN_POINT('Ctrl Pts',(185.231676812499,5.12964958327893,332.517857060067));
#7531=CARTESIAN_POINT('Ctrl Pts',(185.231676812499,5.12178078536785,332.497609729186));
#7532=CARTESIAN_POINT('Ctrl Pts',(185.231676812499,5.06280079278511,332.34584735853));
#7533=CARTESIAN_POINT('Ctrl Pts',(185.231676812499,4.99745588381262,332.196865405903));
#7534=CARTESIAN_POINT('Ctrl Pts',(185.231676812499,4.92604289876815,332.051036300688));
#7535=CARTESIAN_POINT('Ctrl Pts',(185.231676812499,4.85395352364228,331.903825971033));
#7536=CARTESIAN_POINT('Ctrl Pts',(185.231676812499,4.77568040330955,331.759827788406));
#7537=CARTESIAN_POINT('Ctrl Pts',(185.231676812499,4.69147536577344,331.619427723857));
#7538=CARTESIAN_POINT('Ctrl Pts',(185.231676812499,4.60716592630847,331.478853583766));
#7539=CARTESIAN_POINT('Ctrl Pts',(185.231676812499,4.5169096000525,331.341885760191));
#7540=CARTESIAN_POINT('Ctrl Pts',(185.231676812499,4.4209090797894,331.208925334346));
#7541=CARTESIAN_POINT('Ctrl Pts',(185.231676812499,4.35701600287431,331.120433618968));
#7542=CARTESIAN_POINT('Ctrl Pts',(185.231676812499,4.29057747731511,331.033717298733));
#7543=CARTESIAN_POINT('Ctrl Pts',(185.231676812499,4.22164182107164,330.948900409606));
#7544=CARTESIAN_POINT('Ctrl Pts',(185.231676812499,4.18078803288743,330.898634822657));
#7545=CARTESIAN_POINT('Ctrl Pts',(185.231676812499,4.13905703477076,330.849036452026));
#7546=CARTESIAN_POINT('Ctrl Pts',(185.231676812499,4.09647004598961,330.80012006803));
#7547=CARTESIAN_POINT('Ctrl Pts',(185.231676812499,4.06686009781426,330.766109408049));
#7548=CARTESIAN_POINT('Ctrl Pts',(185.231676812499,4.03683632805114,330.732428447414));
#7549=CARTESIAN_POINT('Ctrl Pts',(185.231676812499,4.00640559299697,330.69908238668));
#7550=CARTESIAN_POINT('Ctrl Pts',(185.231676812499,3.99119933337399,330.682419336773));
#7551=CARTESIAN_POINT('Ctrl Pts',(185.231676812499,3.97588993501583,330.665838295175));
#7552=CARTESIAN_POINT('Ctrl Pts',(185.231676812499,3.96048314632903,330.649345180255));
#7553=CARTESIAN_POINT('Ctrl Pts',(185.231676812499,3.84539202131251,330.526139028103));
#7554=CARTESIAN_POINT('Ctrl Pts',(185.231676812499,3.72508679254122,330.408066830259));
#7555=CARTESIAN_POINT('Ctrl Pts',(185.231676812499,3.60001757347812,330.295335573318));
#7556=CARTESIAN_POINT('Ctrl Pts',(185.231676812499,3.47494835441503,330.182604316378));
#7557=CARTESIAN_POINT('Ctrl Pts',(185.231676812499,3.34511458049823,330.075213491582));
#7558=CARTESIAN_POINT('Ctrl Pts',(185.231676812499,3.21091932475301,329.973398455747));
#7559=CARTESIAN_POINT('Ctrl Pts',(185.231676812499,3.15167027138406,329.928445715366));
#7560=CARTESIAN_POINT('Ctrl Pts',(185.231676812499,3.09157045089737,329.884580305075));
#7561=CARTESIAN_POINT('Ctrl Pts',(185.231676812499,3.03065207423348,329.841824638955));
#7562=CARTESIAN_POINT('Ctrl Pts',(185.231676812499,2.98416479193989,329.809197460928));
#7563=CARTESIAN_POINT('Ctrl Pts',(185.231676812499,2.93720080625702,329.777216550693));
#7564=CARTESIAN_POINT('Ctrl Pts',(185.231676812499,2.8897739093974,329.745892454179));
#7565=CARTESIAN_POINT('Ctrl Pts',(185.231676812499,2.86904115537433,329.732199068547));
#7566=CARTESIAN_POINT('Ctrl Pts',(185.231676812499,2.84822276624274,329.718633121031));
#7567=CARTESIAN_POINT('Ctrl Pts',(185.231676812499,2.82732709096244,329.705199893148));
#7568=CARTESIAN_POINT('Ctrl Pts',(185.231676812499,2.68375632121808,329.612902379839));
#7569=CARTESIAN_POINT('Ctrl Pts',(185.231676812499,2.53644282832064,329.526803017701));
#7570=CARTESIAN_POINT('Ctrl Pts',(185.231676812499,2.38580446285762,329.447132130605));
#7571=CARTESIAN_POINT('Ctrl Pts',(185.231676812499,2.23563497383018,329.367709226826));
#7572=CARTESIAN_POINT('Ctrl Pts',(185.231676812499,2.08216068135469,329.294674353791));
#7573=CARTESIAN_POINT('Ctrl Pts',(185.231676812499,1.92575956440724,329.228292618111));
#7574=CARTESIAN_POINT('Ctrl Pts',(185.231676812499,1.90861073917047,329.221014097303));
#7575=CARTESIAN_POINT('Ctrl Pts',(185.231676812499,1.89142669618393,329.213815603767));
#7576=CARTESIAN_POINT('Ctrl Pts',(185.231676812499,1.87420791206738,329.206697518036));
#7577=CARTESIAN_POINT('Ctrl Pts',(185.231676812499,1.77690397932603,329.166472974276));
#7578=CARTESIAN_POINT('Ctrl Pts',(185.231676812499,1.67849090257524,329.128815625578));
#7579=CARTESIAN_POINT('Ctrl Pts',(185.231676812499,1.57907388322304,329.093732219127));
#7580=CARTESIAN_POINT('',(182.258435337963,-4.41716094758247,337.622001091848));
#7581=CARTESIAN_POINT('Ctrl Pts',(182.258477686866,-4.41710803447555,337.621844669693));
#7582=CARTESIAN_POINT('Ctrl Pts',(182.349960492498,-4.70739653859804,337.376661777648));
#7583=CARTESIAN_POINT('Ctrl Pts',(182.440441383438,-4.97446109536007,337.095107460796));
#7584=CARTESIAN_POINT('Ctrl Pts',(182.568982327825,-5.33380935274516,336.568720006854));
#7585=CARTESIAN_POINT('Ctrl Pts',(182.614744225292,-5.45551217225447,336.341694783932));
#7586=CARTESIAN_POINT('Ctrl Pts',(182.670714469732,-5.59449636699666,335.964114480957));
#7587=CARTESIAN_POINT('Ctrl Pts',(182.687574387585,-5.63385575200452,335.824697776433));
#7588=CARTESIAN_POINT('Ctrl Pts',(182.706239595221,-5.6731353981708,335.620282861155));
#7589=CARTESIAN_POINT('Ctrl Pts',(182.711142624749,-5.68272605401884,335.558138683474));
#7590=CARTESIAN_POINT('Ctrl Pts',(182.716919714594,-5.69283968382394,335.470904937064));
#7591=CARTESIAN_POINT('Ctrl Pts',(182.718435698403,-5.69533642365568,335.446158968727));
#7592=CARTESIAN_POINT('Ctrl Pts',(182.720459401172,-5.69842158081797,335.41019580278));
#7593=CARTESIAN_POINT('Ctrl Pts',(182.721063514815,-5.69930484271052,335.399014218728));
#7594=CARTESIAN_POINT('Ctrl Pts',(182.722057144062,-5.70069009110022,335.379824532242));
#7595=CARTESIAN_POINT('Ctrl Pts',(182.722458743629,-5.70122898255233,335.371820293223));
#7596=CARTESIAN_POINT('Ctrl Pts',(182.723251756172,-5.70224885894303,335.355491589503));
#7597=CARTESIAN_POINT('Ctrl Pts',(182.723642136471,-5.70272672527546,335.347167209565));
#7598=CARTESIAN_POINT('Ctrl Pts',(182.724577978155,-5.70380994661762,335.326474111663));
#7599=CARTESIAN_POINT('Ctrl Pts',(182.725106794512,-5.70436469462718,335.314102744529));
#7600=CARTESIAN_POINT('Ctrl Pts',(182.726971316045,-5.70609320273036,335.26779388918));
#7601=CARTESIAN_POINT('Ctrl Pts',(182.728107592672,-5.70666173958303,335.233838419053));
#7602=CARTESIAN_POINT('Ctrl Pts',(182.731015334075,-5.7062376554595,335.124764542842));
#7603=CARTESIAN_POINT('Ctrl Pts',(182.731884562569,-5.70252219120966,335.049775454453));
#7604=CARTESIAN_POINT('Ctrl Pts',(182.731029638564,-5.67813275898276,334.793468251929));
#7605=CARTESIAN_POINT('Ctrl Pts',(182.723830789714,-5.64105770048092,334.615488743082));
#7606=CARTESIAN_POINT('Ctrl Pts',(182.692813006775,-5.50897328499186,334.199640387766));
#7607=CARTESIAN_POINT('Ctrl Pts',(182.663869070168,-5.39824504733339,333.970817760501));
#7608=CARTESIAN_POINT('Ctrl Pts',(182.593220142657,-5.13036614653951,333.550186573158));
#7609=CARTESIAN_POINT('Ctrl Pts',(182.552104916986,-4.97514574927775,333.358657311859));
#7610=CARTESIAN_POINT('Ctrl Pts',(182.508320087374,-4.80500519224339,333.183282451721));
#7611=CARTESIAN_POINT('Ctrl Pts',(181.756492029768,3.56482183513016,338.698411259755));
#7612=CARTESIAN_POINT('Ctrl Pts',(181.764934144517,3.45271479600097,338.806468907455));
#7613=CARTESIAN_POINT('Ctrl Pts',(181.773376259266,3.33571674076433,338.909401826378));
#7614=CARTESIAN_POINT('Ctrl Pts',(181.781818374015,3.2143022604258,339.006801909394));
#7615=CARTESIAN_POINT('Ctrl Pts',(181.78720325498,3.13685691130715,339.068929453096));
#7616=CARTESIAN_POINT('Ctrl Pts',(181.792588135945,3.05761537103361,339.128806670922));
#7617=CARTESIAN_POINT('Ctrl Pts',(181.79797301691,2.97670766664917,339.186336349341));
#7618=CARTESIAN_POINT('Ctrl Pts',(181.806031590385,2.85562779789292,339.272430571956));
#7619=CARTESIAN_POINT('Ctrl Pts',(181.81409016386,2.73078611467066,339.353285532255));
#7620=CARTESIAN_POINT('Ctrl Pts',(181.822148737336,2.60265733937138,339.428586155458));
#7621=CARTESIAN_POINT('Ctrl Pts',(181.830205583936,2.474556020847,339.503870642456));
#7622=CARTESIAN_POINT('Ctrl Pts',(181.838262430535,2.34316930203407,339.573602998336));
#7623=CARTESIAN_POINT('Ctrl Pts',(181.846319277135,2.20899874841433,339.637512813136));
#7624=CARTESIAN_POINT('Ctrl Pts',(181.854376313082,2.07482504159838,339.701424129907));
#7625=CARTESIAN_POINT('Ctrl Pts',(181.862433349029,1.93786766757888,339.759512485029));
#7626=CARTESIAN_POINT('Ctrl Pts',(181.870490384976,1.79865101653544,339.811554331317));
#7627=CARTESIAN_POINT('Ctrl Pts',(181.878546931079,1.65944282945296,339.863593013615));
#7628=CARTESIAN_POINT('Ctrl Pts',(181.886603477182,1.51797595199898,339.909585806759));
#7629=CARTESIAN_POINT('Ctrl Pts',(181.894660023285,1.37479288358573,339.949358048246));
#7630=CARTESIAN_POINT('Ctrl Pts',(181.90271854851,1.2315746416961,339.98914005994));
#7631=CARTESIAN_POINT('Ctrl Pts',(181.910777073734,1.08663968699248,340.022698377151));
#7632=CARTESIAN_POINT('Ctrl Pts',(181.918835598959,0.940544380227419,340.049908596333));
#7633=CARTESIAN_POINT('Ctrl Pts',(181.924330788884,0.840920511667451,340.068463520234));
#7634=CARTESIAN_POINT('Ctrl Pts',(181.929825978809,0.740757356148767,340.084067618826));
#7635=CARTESIAN_POINT('Ctrl Pts',(181.935321168733,0.640233743136665,340.096695136718));
#7636=CARTESIAN_POINT('Ctrl Pts',(181.9433976224,0.492491023764222,340.115254197386));
#7637=CARTESIAN_POINT('Ctrl Pts',(181.951474076068,0.343915819091288,340.127387947124));
#7638=CARTESIAN_POINT('Ctrl Pts',(181.959550529735,0.195078012643335,340.133044431084));
#7639=CARTESIAN_POINT('Ctrl Pts',(181.967625476531,0.0462679757346483,340.13869985968));
#7640=CARTESIAN_POINT('Ctrl Pts',(181.975700423327,-0.102804235986503,340.137880421174));
#7641=CARTESIAN_POINT('Ctrl Pts',(181.983775370123,-0.251566345801858,340.130586217593));
#7642=CARTESIAN_POINT('Ctrl Pts',(181.991850664336,-0.400334855969035,340.123291700186));
#7643=CARTESIAN_POINT('Ctrl Pts',(181.999925958549,-0.548792908144701,340.109521873129));
#7644=CARTESIAN_POINT('Ctrl Pts',(182.008001252762,-0.696370379884273,340.089328920056));
#7645=CARTESIAN_POINT('Ctrl Pts',(182.016076104672,-0.84393976846008,340.069137072998));
#7646=CARTESIAN_POINT('Ctrl Pts',(182.024150956582,-0.990628346638582,340.042522849499));
#7647=CARTESIAN_POINT('Ctrl Pts',(182.032225808493,-1.13587323525567,340.00959005867));
#7648=CARTESIAN_POINT('Ctrl Pts',(182.040302551253,-1.28115213519398,339.976649556123));
#7649=CARTESIAN_POINT('Ctrl Pts',(182.048379294014,-1.42498634838971,339.937387602384));
#7650=CARTESIAN_POINT('Ctrl Pts',(182.056456036775,-1.56682461334312,339.891958829909));
#7651=CARTESIAN_POINT('Ctrl Pts',(182.061860464702,-1.66173350210462,339.861560867026));
#7652=CARTESIAN_POINT('Ctrl Pts',(182.06726489263,-1.75574897728243,339.828402813942));
#7653=CARTESIAN_POINT('Ctrl Pts',(182.072669320557,-1.84870995570134,339.792543381357));
#7654=CARTESIAN_POINT('Ctrl Pts',(182.080740085132,-1.98753430151757,339.73899228546));
#7655=CARTESIAN_POINT('Ctrl Pts',(182.088810849707,-2.12405523137392,339.679395580914));
#7656=CARTESIAN_POINT('Ctrl Pts',(182.096881614282,-2.25774675738525,339.613976608308));
#7657=CARTESIAN_POINT('Ctrl Pts',(182.104950790195,-2.39141196734384,339.548570512877));
#7658=CARTESIAN_POINT('Ctrl Pts',(182.113019966108,-2.52224858781886,339.477344581109));
#7659=CARTESIAN_POINT('Ctrl Pts',(182.121089142021,-2.64975313097116,339.400569157212));
#7660=CARTESIAN_POINT('Ctrl Pts',(182.129158598995,-2.77726211529379,339.323791059115));
#7661=CARTESIAN_POINT('Ctrl Pts',(182.13722805597,-2.90143850497578,339.241463249543));
#7662=CARTESIAN_POINT('Ctrl Pts',(182.145297512944,-3.02180534132847,339.153900942683));
#7663=CARTESIAN_POINT('Ctrl Pts',(182.153366504103,-3.14216522941335,339.066343690424));
#7664=CARTESIAN_POINT('Ctrl Pts',(182.161435495261,-3.25871573730262,338.973552740628));
#7665=CARTESIAN_POINT('Ctrl Pts',(182.16950448642,-3.37101070813753,338.87588536571));
#7666=CARTESIAN_POINT('Ctrl Pts',(182.177575384854,-3.48333222224721,338.778194905056));
#7667=CARTESIAN_POINT('Ctrl Pts',(182.185646283288,-3.59139593957822,338.67562593289));
#7668=CARTESIAN_POINT('Ctrl Pts',(182.193717181722,-3.6947899848816,338.568574999929));
#7669=CARTESIAN_POINT('Ctrl Pts',(182.199150611942,-3.76439615510316,338.496506966996));
#7670=CARTESIAN_POINT('Ctrl Pts',(182.204584042161,-3.83188667994544,338.422408447104));
#7671=CARTESIAN_POINT('Ctrl Pts',(182.21001747238,-3.89714554158373,338.346409596898));
#7672=CARTESIAN_POINT('Ctrl Pts',(182.218340811104,-3.99711399396613,338.229988818981));
#7673=CARTESIAN_POINT('Ctrl Pts',(182.226664149828,-4.09187050337891,338.109076110878));
#7674=CARTESIAN_POINT('Ctrl Pts',(182.234987488552,-4.18103669417411,337.984146900618));
#7675=CARTESIAN_POINT('Ctrl Pts',(182.242803438356,-4.26476733334942,337.866833347875));
#7676=CARTESIAN_POINT('Ctrl Pts',(182.250619388159,-4.34356867268145,337.745978508847));
#7677=CARTESIAN_POINT('Ctrl Pts',(182.258435337963,-4.41716094758247,337.622001091848));
#7678=CARTESIAN_POINT('Ctrl Pts',(181.37007030626,4.28788785758327,332.172095440742));
#7679=CARTESIAN_POINT('Ctrl Pts',(181.328355740759,3.86434819387074,331.529891326477));
#7680=CARTESIAN_POINT('Ctrl Pts',(181.244928279822,2.72375436716049,330.440274865794));
#7681=CARTESIAN_POINT('Ctrl Pts',(181.119787923451,0.473039962656459,329.708131390012));
#7682=CARTESIAN_POINT('Ctrl Pts',(180.99464756708,-1.87184555895904,330.029474338107));
#7683=CARTESIAN_POINT('Ctrl Pts',(180.911220106143,-3.18761322620324,330.899516724865));
#7684=CARTESIAN_POINT('Ctrl Pts',(180.869505540642,-3.7183409627162,331.456418907311));
#7685=CARTESIAN_POINT('Ctrl Pts',(181.558087260742,4.55974375143968,331.992803783117));
#7686=CARTESIAN_POINT('Ctrl Pts',(181.516372695242,4.10935129733558,331.309883358323));
#7687=CARTESIAN_POINT('Ctrl Pts',(181.432945234305,2.89644281021763,330.151184247459));
#7688=CARTESIAN_POINT('Ctrl Pts',(181.307804877934,0.503031115911629,329.372622225845));
#7689=CARTESIAN_POINT('Ctrl Pts',(181.182664521562,-1.99052222786772,329.714338601904));
#7690=CARTESIAN_POINT('Ctrl Pts',(181.099237060626,-3.38971073240211,330.639542447777));
#7691=CARTESIAN_POINT('Ctrl Pts',(181.057522495125,-3.95408707820623,331.231752722606));
#7692=CARTESIAN_POINT('Ctrl Pts',(181.746104215225,4.83159964529608,331.813512125491));
#7693=CARTESIAN_POINT('Ctrl Pts',(181.704389649724,4.35435440080044,331.089875390168));
#7694=CARTESIAN_POINT('Ctrl Pts',(181.620962188788,3.06913125327478,329.862093629124));
#7695=CARTESIAN_POINT('Ctrl Pts',(181.495821832417,0.533022269166806,329.037113061678));
#7696=CARTESIAN_POINT('Ctrl Pts',(181.370681476045,-2.1091988967764,329.399202865703));
#7697=CARTESIAN_POINT('Ctrl Pts',(181.287254015109,-3.59180823860098,330.37956817069));
#7698=CARTESIAN_POINT('Ctrl Pts',(181.245539449608,-4.18983319369624,331.007086537901));
#7699=CARTESIAN_POINT('Ctrl Pts',(181.934121169709,5.1034555391525,331.634220467866));
#7700=CARTESIAN_POINT('Ctrl Pts',(181.892406604207,4.59935750426528,330.869867422015));
#7701=CARTESIAN_POINT('Ctrl Pts',(181.808979143271,3.24181969633193,329.573003010789));
#7702=CARTESIAN_POINT('Ctrl Pts',(181.6838387869,0.563013422421977,328.70160389751));
#7703=CARTESIAN_POINT('Ctrl Pts',(181.558698430529,-2.22787556568508,329.084067129501));
#7704=CARTESIAN_POINT('Ctrl Pts',(181.475270969592,-3.79390574479985,330.119593893603));
#7705=CARTESIAN_POINT('Ctrl Pts',(181.433556404091,-4.42557930918627,330.782420353195));
#7706=CARTESIAN_POINT('',(180.993849537574,-1.82724795145699,330.199232823142));
#7707=CARTESIAN_POINT('Ctrl Pts',(181.433471471437,-4.42539066683718,330.782448221021));
#7708=CARTESIAN_POINT('Ctrl Pts',(181.335375473532,-4.01063179047883,330.638200736283));
#7709=CARTESIAN_POINT('Ctrl Pts',(181.245907584842,-3.58266997347834,330.517361513033));
#7710=CARTESIAN_POINT('Ctrl Pts',(181.096214561382,-2.71608572687693,330.323224835212));
#7711=CARTESIAN_POINT('Ctrl Pts',(181.03528545648,-2.27326928320113,330.248969261106));
#7712=CARTESIAN_POINT('Ctrl Pts',(180.993969721933,-1.82720031248029,330.19937707939));
#7713=CARTESIAN_POINT('',(181.235953224802,2.48747578839151,330.505707534587));
#7714=CARTESIAN_POINT('Ctrl Pts',(181.236066270803,2.48739342482026,330.505858565532));
#7715=CARTESIAN_POINT('Ctrl Pts',(181.329278473347,2.95503192785205,330.630394558558));
#7716=CARTESIAN_POINT('Ctrl Pts',(181.439439013854,3.40978123839685,330.785458718465));
#7717=CARTESIAN_POINT('Ctrl Pts',(181.676346524597,4.28251791449889,331.157496738812));
#7718=CARTESIAN_POINT('Ctrl Pts',(181.805383790547,4.70817800168015,331.378046456073));
#7719=CARTESIAN_POINT('Ctrl Pts',(181.93402621666,5.10326494491035,331.634214435745));
#7720=CARTESIAN_POINT('Ctrl Pts',(180.993842605595,-1.82717158359009,330.199203757019));
#7721=CARTESIAN_POINT('Ctrl Pts',(180.99417094369,-1.82151293100644,330.197050087361));
#7722=CARTESIAN_POINT('Ctrl Pts',(180.994499281784,-1.81585046631374,330.194906420758));
#7723=CARTESIAN_POINT('Ctrl Pts',(180.994827619879,-1.81018422265156,330.192772769822));
#7724=CARTESIAN_POINT('Ctrl Pts',(181.002908535245,-1.67072908100198,330.140260274553));
#7725=CARTESIAN_POINT('Ctrl Pts',(181.010989450612,-1.52897030831888,330.093813700451));
#7726=CARTESIAN_POINT('Ctrl Pts',(181.019070365978,-1.38545129924182,330.05361493008));
#7727=CARTESIAN_POINT('Ctrl Pts',(181.027478360995,-1.23612327655373,330.011789091589));
#7728=CARTESIAN_POINT('Ctrl Pts',(181.035886356013,-1.08488989577882,329.97672753868));
#7729=CARTESIAN_POINT('Ctrl Pts',(181.04429435103,-0.932379817120784,329.948577582589));
#7730=CARTESIAN_POINT('Ctrl Pts',(181.052374953363,-0.785808215333428,329.921523736765));
#7731=CARTESIAN_POINT('Ctrl Pts',(181.060455555697,-0.638057813713283,329.900853427042));
#7732=CARTESIAN_POINT('Ctrl Pts',(181.06853615803,-0.489696403519162,329.886645133097));
#7733=CARTESIAN_POINT('Ctrl Pts',(181.076616788472,-0.341334477244848,329.872436789728));
#7734=CARTESIAN_POINT('Ctrl Pts',(181.084697418914,-0.192361865645472,329.864690534929));
#7735=CARTESIAN_POINT('Ctrl Pts',(181.092778049357,-0.0433509756674483,
329.863432930895));
#7736=CARTESIAN_POINT('Ctrl Pts',(181.10086036639,0.105691015909345,329.862175064374));
#7737=CARTESIAN_POINT('Ctrl Pts',(181.108942683424,0.254770973150995,329.867408554713));
#7738=CARTESIAN_POINT('Ctrl Pts',(181.117025000458,0.403316444216384,329.879107850352));
#7739=CARTESIAN_POINT('Ctrl Pts',(181.1180054357,0.421335932225548,329.880527047558));
#7740=CARTESIAN_POINT('Ctrl Pts',(181.118985870942,0.439347559076759,329.882041327492));
#7741=CARTESIAN_POINT('Ctrl Pts',(181.119966306184,0.457350306861083,329.88365059253));
#7742=CARTESIAN_POINT('Ctrl Pts',(181.128037500542,0.605553543663938,329.89689847504));
#7743=CARTESIAN_POINT('Ctrl Pts',(181.1361086949,0.753208183541544,329.91659254913));
#7744=CARTESIAN_POINT('Ctrl Pts',(181.144179889258,0.899747050476711,329.942663170437));
#7745=CARTESIAN_POINT('Ctrl Pts',(181.152250191989,1.0462697292173,329.968730911714));
#7746=CARTESIAN_POINT('Ctrl Pts',(181.160320494719,1.19167655492713,330.001173740569));
#7747=CARTESIAN_POINT('Ctrl Pts',(181.16839079745,1.3354088573094,330.039870591777));
#7748=CARTESIAN_POINT('Ctrl Pts',(181.176459923976,1.47912021145519,330.07856180312));
#7749=CARTESIAN_POINT('Ctrl Pts',(181.184529050502,1.62115721050249,330.123505130563));
#7750=CARTESIAN_POINT('Ctrl Pts',(181.192598177028,1.76097459482369,330.174529138117));
#7751=CARTESIAN_POINT('Ctrl Pts',(181.200668287031,1.90080902029365,330.225559364551));
#7752=CARTESIAN_POINT('Ctrl Pts',(181.208738397034,2.038422979052,330.282671640769));
#7753=CARTESIAN_POINT('Ctrl Pts',(181.216808507037,2.17328891739442,330.345645496524));
#7754=CARTESIAN_POINT('Ctrl Pts',(181.223180833583,2.27978186467651,330.395370961556));
#7755=CARTESIAN_POINT('Ctrl Pts',(181.22955316013,2.38456171924082,330.448750140761));
#7756=CARTESIAN_POINT('Ctrl Pts',(181.235925486676,2.48737852733284,330.505653704457));
#7757=CARTESIAN_POINT('Ctrl Pts',(180.751352012451,-3.51522511306203,339.536198064046));
#7758=CARTESIAN_POINT('Ctrl Pts',(180.712625990112,-2.88450494225346,340.024960537033));
#7759=CARTESIAN_POINT('Ctrl Pts',(180.622265271322,-1.17144813710853,340.854840788682));
#7760=CARTESIAN_POINT('Ctrl Pts',(180.531904552531,0.760780206681846,340.786796970132));
#7761=CARTESIAN_POINT('Ctrl Pts',(180.48026985608,1.77266279316809,340.458165176456));
#7762=CARTESIAN_POINT('Ctrl Pts',(180.82341369046,-3.59167846941827,339.634856771792));
#7763=CARTESIAN_POINT('Ctrl Pts',(180.784687668121,-2.94724063546469,340.134249440661));
#7764=CARTESIAN_POINT('Ctrl Pts',(180.694326949331,-1.19692620437268,340.98217892915));
#7765=CARTESIAN_POINT('Ctrl Pts',(180.60396623054,0.777326572385168,340.91265521155));
#7766=CARTESIAN_POINT('Ctrl Pts',(180.552331534089,1.81121680204847,340.576875937179));
#7767=CARTESIAN_POINT('Ctrl Pts',(180.895475368468,-3.66813182577451,339.733515479539));
#7768=CARTESIAN_POINT('Ctrl Pts',(180.85674934613,-3.00997632867591,340.24353834429));
#7769=CARTESIAN_POINT('Ctrl Pts',(180.766388627339,-1.22240427163682,341.109517069619));
#7770=CARTESIAN_POINT('Ctrl Pts',(180.676027908549,0.79387293808849,341.038513452968));
#7771=CARTESIAN_POINT('Ctrl Pts',(180.624393212098,1.84977081092886,340.695586697903));
#7772=CARTESIAN_POINT('Ctrl Pts',(180.967537046477,-3.74458518213076,339.832174187285));
#7773=CARTESIAN_POINT('Ctrl Pts',(180.928811024139,-3.07271202188714,340.352827247918));
#7774=CARTESIAN_POINT('Ctrl Pts',(180.838450305348,-1.24788233890097,341.236855210088));
#7775=CARTESIAN_POINT('Ctrl Pts',(180.748089586558,0.810419303791811,341.164371694386));
#7776=CARTESIAN_POINT('Ctrl Pts',(180.696454890107,1.88832481980924,340.814297458627));
#7777=CARTESIAN_POINT('Ctrl Pts',(180.696529438166,-2.55854249889813,340.136670690217));
#7778=CARTESIAN_POINT('Ctrl Pts',(180.73617790029,-2.7597370763773,340.0944890875));
#7779=CARTESIAN_POINT('Ctrl Pts',(180.778964893207,-2.95961823467644,340.047992945047));
#7780=CARTESIAN_POINT('Ctrl Pts',(180.869583792205,-3.35496090197214,339.94657615533));
#7781=CARTESIAN_POINT('Ctrl Pts',(180.917495527076,-3.55084795862925,339.891574190277));
#7782=CARTESIAN_POINT('Ctrl Pts',(180.967537046477,-3.74458518213073,339.832174187285));
#7783=CARTESIAN_POINT('Ctrl Pts',(181.135238634734,-4.11718022388969,339.518921605947));
#7784=CARTESIAN_POINT('Ctrl Pts',(181.073326230095,-3.11267730650807,340.434139400932));
#7785=CARTESIAN_POINT('Ctrl Pts',(180.949524158232,-0.47430519230716,341.565277535024));
#7786=CARTESIAN_POINT('Ctrl Pts',(180.825722086368,2.29912071323036,340.825045741512));
#7787=CARTESIAN_POINT('Ctrl Pts',(180.763832419144,3.42440815596409,340.064114369154));
#7788=CARTESIAN_POINT('Ctrl Pts',(181.323574328469,-3.89748481312009,339.277789014107));
#7789=CARTESIAN_POINT('Ctrl Pts',(181.261661923831,-2.94658282381369,340.144170193138));
#7790=CARTESIAN_POINT('Ctrl Pts',(181.137859851967,-0.448995959194304,341.214950061744));
#7791=CARTESIAN_POINT('Ctrl Pts',(181.014057780104,2.17643813874135,340.514217517499));
#7792=CARTESIAN_POINT('Ctrl Pts',(180.952168112879,3.24167951268005,339.793889937379));
#7793=CARTESIAN_POINT('Ctrl Pts',(181.511910022206,-3.6777894023505,339.036656422269));
#7794=CARTESIAN_POINT('Ctrl Pts',(181.449997617566,-2.78048834111931,339.854200985343));
#7795=CARTESIAN_POINT('Ctrl Pts',(181.326195545702,-0.423686726081443,340.864622588464));
#7796=CARTESIAN_POINT('Ctrl Pts',(181.202393473839,2.05375556425234,340.203389293486));
#7797=CARTESIAN_POINT('Ctrl Pts',(181.140503806615,3.05895086939599,339.523665505604));
#7798=CARTESIAN_POINT('Ctrl Pts',(181.700245715941,-3.45809399158091,338.795523830431));
#7799=CARTESIAN_POINT('Ctrl Pts',(181.638333311301,-2.61439385842493,339.564231777549));
#7800=CARTESIAN_POINT('Ctrl Pts',(181.514531239438,-0.398377492968587,340.514295115184));
#7801=CARTESIAN_POINT('Ctrl Pts',(181.390729167575,1.93107298976333,339.892561069473));
#7802=CARTESIAN_POINT('Ctrl Pts',(181.328839500351,2.87622222611195,339.253441073828));
#7803=CARTESIAN_POINT('',(181.337571198602,2.72350574788935,339.355309059494));
#7804=CARTESIAN_POINT('Ctrl Pts',(181.337515959362,2.723475111057,339.355310357786));
#7805=CARTESIAN_POINT('Ctrl Pts',(181.241203275559,2.82033438186087,339.490333974197));
#7806=CARTESIAN_POINT('Ctrl Pts',(181.144706554227,2.92995105049118,339.616169622604));
#7807=CARTESIAN_POINT('Ctrl Pts',(180.953497167844,3.16562337980582,339.851156463483));
#7808=CARTESIAN_POINT('Ctrl Pts',(180.85798168447,3.2926517407027,339.961263535214));
#7809=CARTESIAN_POINT('Ctrl Pts',(180.763832419144,3.4244081559647,340.064114369153));
#7810=CARTESIAN_POINT('',(181.698952960354,-3.45859239216069,338.797938813013));
#7811=CARTESIAN_POINT('Ctrl Pts',(181.698952960354,-3.45859239215945,338.797938813014));
#7812=CARTESIAN_POINT('Ctrl Pts',(181.690923324486,-3.349099573853,338.897648431055));
#7813=CARTESIAN_POINT('Ctrl Pts',(181.682893688618,-3.23526892443982,338.99264087084));
#7814=CARTESIAN_POINT('Ctrl Pts',(181.674864052751,-3.11753099767851,339.082548351338));
#7815=CARTESIAN_POINT('Ctrl Pts',(181.666835946353,-2.99981549741501,339.172438706429));
#7816=CARTESIAN_POINT('Ctrl Pts',(181.658807839955,-2.87819447181031,339.257245829385));
#7817=CARTESIAN_POINT('Ctrl Pts',(181.650779733557,-2.75313052873629,339.336643039753));
#7818=CARTESIAN_POINT('Ctrl Pts',(181.642752285051,-2.62807683447564,339.416033743633));
#7819=CARTESIAN_POINT('Ctrl Pts',(181.634724836545,-2.49958107022608,339.49001523899));
#7820=CARTESIAN_POINT('Ctrl Pts',(181.626697388039,-2.3681339250979,339.558304758932));
#7821=CARTESIAN_POINT('Ctrl Pts',(181.618669726312,-2.23668328853949,339.626596092744));
#7822=CARTESIAN_POINT('Ctrl Pts',(181.610642064586,-2.10228141428578,339.689194995255));
#7823=CARTESIAN_POINT('Ctrl Pts',(181.602614402859,-1.96544285195621,339.745865037924));
#7824=CARTESIAN_POINT('Ctrl Pts',(181.594583330202,-1.82854614732993,339.802559159526));
#7825=CARTESIAN_POINT('Ctrl Pts',(181.586552257546,-1.68921099663222,339.853319256526));
#7826=CARTESIAN_POINT('Ctrl Pts',(181.57852118489,-1.54797184628561,339.897957097159));
#7827=CARTESIAN_POINT('Ctrl Pts',(181.570488744678,-1.40670864529598,339.942602538862));
#7828=CARTESIAN_POINT('Ctrl Pts',(181.562456304465,-1.26354112110727,339.981123548396));
#7829=CARTESIAN_POINT('Ctrl Pts',(181.554423864253,-1.11901844459552,340.013381920735));
#7830=CARTESIAN_POINT('Ctrl Pts',(181.54638628216,-0.974403253435857,340.045660942927));
#7831=CARTESIAN_POINT('Ctrl Pts',(181.538348700066,-0.828431506451216,340.071669246487));
#7832=CARTESIAN_POINT('Ctrl Pts',(181.530311117973,-0.681662966543317,340.091319687718));
#7833=CARTESIAN_POINT('Ctrl Pts',(181.524635398209,-0.578022705946049,340.105195800754));
#7834=CARTESIAN_POINT('Ctrl Pts',(181.518959678445,-0.473985336372291,340.115902674231));
#7835=CARTESIAN_POINT('Ctrl Pts',(181.513283958681,-0.369749448980302,340.123425212441));
#7836=CARTESIAN_POINT('Ctrl Pts',(181.505278951843,-0.22273567346082,340.134034962801));
#7837=CARTESIAN_POINT('Ctrl Pts',(181.497273945005,-0.0751969877806426,
340.138317571497));
#7838=CARTESIAN_POINT('Ctrl Pts',(181.489268938167,0.072306158600289,340.136241075137));
#7839=CARTESIAN_POINT('Ctrl Pts',(181.481267916047,0.219735881144422,340.134165612412));
#7840=CARTESIAN_POINT('Ctrl Pts',(181.473266893926,0.367129758108576,340.125737359625));
#7841=CARTESIAN_POINT('Ctrl Pts',(181.465265871806,0.513926528021877,340.110976431788));
#7842=CARTESIAN_POINT('Ctrl Pts',(181.45726784588,0.660668325990168,340.096221031572));
#7843=CARTESIAN_POINT('Ctrl Pts',(181.449269819954,0.806813122657021,340.075137718697));
#7844=CARTESIAN_POINT('Ctrl Pts',(181.441271794028,0.951803762915764,340.047798545841));
#7845=CARTESIAN_POINT('Ctrl Pts',(181.433275778068,1.0967579659101,340.02046624353));
#7846=CARTESIAN_POINT('Ctrl Pts',(181.425279762108,1.2405582549564,339.986881280004));
#7847=CARTESIAN_POINT('Ctrl Pts',(181.417283746148,1.38265646389062,339.94716703431));
#7848=CARTESIAN_POINT('Ctrl Pts',(181.409287738572,1.52475452381916,339.907452830261));
#7849=CARTESIAN_POINT('Ctrl Pts',(181.401291730997,1.66515017650093,339.861609444636));
#7850=CARTESIAN_POINT('Ctrl Pts',(181.393295723421,1.8033088432631,339.809810576136));
#7851=CARTESIAN_POINT('Ctrl Pts',(181.385300004087,1.94146252965741,339.75801357489));
#7852=CARTESIAN_POINT('Ctrl Pts',(181.377304284753,2.07737907176908,339.700261642185));
#7853=CARTESIAN_POINT('Ctrl Pts',(181.369308565419,2.21054241446942,339.636777199341));
#7854=CARTESIAN_POINT('Ctrl Pts',(181.361310820325,2.34373949485135,339.573276672357));
#7855=CARTESIAN_POINT('Ctrl Pts',(181.35331307523,2.4741816741913,339.504040882687));
#7856=CARTESIAN_POINT('Ctrl Pts',(181.345315330136,2.60137568129605,339.429339129855));
#7857=CARTESIAN_POINT('Ctrl Pts',(181.342733952958,2.64242921616399,339.405228158871));
#7858=CARTESIAN_POINT('Ctrl Pts',(181.34015257578,2.68314456862808,339.380548118814));
#7859=CARTESIAN_POINT('Ctrl Pts',(181.337571198602,2.72350574788935,339.355309059494));
#7860=CARTESIAN_POINT('Ctrl Pts',(181.127180420915,-3.98468371561092,339.636058369257));
#7861=CARTESIAN_POINT('Ctrl Pts',(181.229310902963,-3.86352131576755,339.506182820355));
#7862=CARTESIAN_POINT('Ctrl Pts',(181.332333550813,-3.75334228949432,339.366387183163));
#7863=CARTESIAN_POINT('Ctrl Pts',(181.524375317495,-3.5785839673492,339.083778531583));
#7864=CARTESIAN_POINT('Ctrl Pts',(181.612373862498,-3.51097495739658,338.945369027672));
#7865=CARTESIAN_POINT('Ctrl Pts',(181.698952960354,-3.45859239216168,338.797938813012));
#7866=CARTESIAN_POINT('Origin',(175.231676812499,0.,335.));
#7867=CARTESIAN_POINT('',(167.731676812499,-45.,335.));
#7868=CARTESIAN_POINT('Origin',(175.231676812499,-45.,335.));
#7869=CARTESIAN_POINT('',(167.731676812499,-6.,335.));
#7870=CARTESIAN_POINT('',(167.731676812499,0.,335.));
#7871=CARTESIAN_POINT('',(170.731676812499,-4.5102810375397E-15,341.));
#7872=CARTESIAN_POINT('Ctrl Pts',(167.731676812499,-6.,335.));
#7873=CARTESIAN_POINT('Ctrl Pts',(167.731676812499,-6.,335.794780989626));
#7874=CARTESIAN_POINT('Ctrl Pts',(167.867335546256,-5.8328999714949,336.617370842401));
#7875=CARTESIAN_POINT('Ctrl Pts',(168.353029590474,-5.20624497170395,338.087656141906));
#7876=CARTESIAN_POINT('Ctrl Pts',(168.700147512561,-4.74828751391861,338.73699386032));
#7877=CARTESIAN_POINT('Ctrl Pts',(169.405023834711,-3.7207625323499,339.764518841889));
#7878=CARTESIAN_POINT('Ctrl Pts',(169.821017677781,-3.07201535485506,340.213611135601));
#7879=CARTESIAN_POINT('Ctrl Pts',(170.323412633441,-1.98596758305952,340.675445953647));
#7880=CARTESIAN_POINT('Ctrl Pts',(170.469308053014,-1.60462674459781,340.795420777217));
#7881=CARTESIAN_POINT('Ctrl Pts',(170.67398081842,-0.816861849349986,340.957723184693));
#7882=CARTESIAN_POINT('Ctrl Pts',(170.731676812499,-0.410146780646359,341.));
#7883=CARTESIAN_POINT('Ctrl Pts',(170.731676812499,-2.63677968348475E-15,
341.));
#7884=CARTESIAN_POINT('',(167.731676812499,6.,335.));
#7885=CARTESIAN_POINT('Ctrl Pts',(170.731676812499,4.02455846426619E-15,
341.));
#7886=CARTESIAN_POINT('Ctrl Pts',(170.731676812499,0.410146780646362,341.));
#7887=CARTESIAN_POINT('Ctrl Pts',(170.67398081842,0.816861849349989,340.957723184693));
#7888=CARTESIAN_POINT('Ctrl Pts',(170.469308053014,1.60462674459781,340.795420777217));
#7889=CARTESIAN_POINT('Ctrl Pts',(170.323412633441,1.98596758305952,340.675445953647));
#7890=CARTESIAN_POINT('Ctrl Pts',(169.821017677781,3.07201535485507,340.213611135601));
#7891=CARTESIAN_POINT('Ctrl Pts',(169.405023834711,3.7207625323499,339.764518841889));
#7892=CARTESIAN_POINT('Ctrl Pts',(168.700147512561,4.74828751391861,338.73699386032));
#7893=CARTESIAN_POINT('Ctrl Pts',(168.353029590474,5.20624497170395,338.087656141906));
#7894=CARTESIAN_POINT('Ctrl Pts',(167.867335546256,5.8328999714949,336.617370842401));
#7895=CARTESIAN_POINT('Ctrl Pts',(167.731676812499,6.,335.794780989626));
#7896=CARTESIAN_POINT('Ctrl Pts',(167.731676812499,6.,335.));
#7897=CARTESIAN_POINT('',(167.731676812499,45.,335.));
#7898=CARTESIAN_POINT('',(167.731676812499,0.,335.));
#7899=CARTESIAN_POINT('Origin',(175.231676812499,45.,335.));
#7900=CARTESIAN_POINT('Ctrl Pts',(167.731676812499,6.00000000000001,335.));
#7901=CARTESIAN_POINT('Ctrl Pts',(167.731676812499,6.00000000000001,334.205219010374));
#7902=CARTESIAN_POINT('Ctrl Pts',(167.867335546256,5.8328999714949,333.382629157599));
#7903=CARTESIAN_POINT('Ctrl Pts',(168.353029590474,5.20624497170395,331.912343858094));
#7904=CARTESIAN_POINT('Ctrl Pts',(168.700147512561,4.74828751391861,331.26300613968));
#7905=CARTESIAN_POINT('Ctrl Pts',(169.405023834711,3.7207625323499,330.235481158111));
#7906=CARTESIAN_POINT('Ctrl Pts',(169.821017677781,3.07201535485507,329.786388864399));
#7907=CARTESIAN_POINT('Ctrl Pts',(170.323412633441,1.98596758305952,329.324554046353));
#7908=CARTESIAN_POINT('Ctrl Pts',(170.469308053014,1.60462674459781,329.204579222783));
#7909=CARTESIAN_POINT('Ctrl Pts',(170.67398081842,0.816861849349989,329.042276815307));
#7910=CARTESIAN_POINT('Ctrl Pts',(170.731676812499,0.410146780646358,329.));
#7911=CARTESIAN_POINT('Ctrl Pts',(170.731676812499,-0.410146780646357,329.));
#7912=CARTESIAN_POINT('Ctrl Pts',(170.67398081842,-0.816861849349986,329.042276815307));
#7913=CARTESIAN_POINT('Ctrl Pts',(170.469308053014,-1.60462674459781,329.204579222783));
#7914=CARTESIAN_POINT('Ctrl Pts',(170.323412633441,-1.98596758305952,329.324554046353));
#7915=CARTESIAN_POINT('Ctrl Pts',(169.821017677781,-3.07201535485506,329.786388864399));
#7916=CARTESIAN_POINT('Ctrl Pts',(169.405023834711,-3.7207625323499,330.235481158111));
#7917=CARTESIAN_POINT('Ctrl Pts',(168.700147512561,-4.74828751391861,331.26300613968));
#7918=CARTESIAN_POINT('Ctrl Pts',(168.353029590474,-5.20624497170395,331.912343858094));
#7919=CARTESIAN_POINT('Ctrl Pts',(167.867335546256,-5.8328999714949,333.382629157599));
#7920=CARTESIAN_POINT('Ctrl Pts',(167.731676812499,-6.,334.205219010374));
#7921=CARTESIAN_POINT('Ctrl Pts',(167.731676812499,-6.,335.));
#7922=CARTESIAN_POINT('Ctrl Pts',(181.698952960354,-3.45859239216063,338.797938813013));
#7923=CARTESIAN_POINT('Ctrl Pts',(181.730827803918,-3.51819566196673,338.74366110459));
#7924=CARTESIAN_POINT('Ctrl Pts',(181.762380948322,-3.57609877279402,338.688362743726));
#7925=CARTESIAN_POINT('Ctrl Pts',(181.953767151073,-3.92184589325217,338.342615623268));
#7926=CARTESIAN_POINT('Ctrl Pts',(182.11679605996,-4.1918704925973,338.001551728627));
#7927=CARTESIAN_POINT('Ctrl Pts',(182.258446931496,-4.41720487047243,337.621927095625));
#7928=CARTESIAN_POINT('Ctrl Pts',(180.993849537574,-1.82724795145699,330.199232823142));
#7929=CARTESIAN_POINT('Ctrl Pts',(180.810080956896,-1.24773913194053,329.978662596696));
#7930=CARTESIAN_POINT('Ctrl Pts',(180.696454890107,-0.616939978405845,329.86325));
#7931=CARTESIAN_POINT('Ctrl Pts',(180.696454890107,0.678169718332449,329.86325));
#7932=CARTESIAN_POINT('Ctrl Pts',(180.835357252731,1.37227470332214,330.003511731902));
#7933=CARTESIAN_POINT('Ctrl Pts',(181.108046445603,2.16628886234032,330.338816012577));
#7934=CARTESIAN_POINT('Ctrl Pts',(181.170594782469,2.32971338705471,330.418390085475));
#7935=CARTESIAN_POINT('Ctrl Pts',(181.235953224802,2.48747578839151,330.505707534587));
#7936=CARTESIAN_POINT('Ctrl Pts',(181.756465142864,3.56497732371045,338.698261381234));
#7937=CARTESIAN_POINT('Ctrl Pts',(181.620014599316,3.31523915334618,338.938999074555));
#7938=CARTESIAN_POINT('Ctrl Pts',(181.475233027865,3.03225184044892,339.162240449674));
#7939=CARTESIAN_POINT('Ctrl Pts',(181.337518659071,2.72350972420708,339.355306572981));
#7940=CARTESIAN_POINT('Origin',(185.231676812499,0.,335.));
#7941=CARTESIAN_POINT('Origin',(185.231676812499,0.,335.));
#7942=CARTESIAN_POINT('Origin',(185.231676812499,0.,335.));
#7943=CARTESIAN_POINT('',(165.231676812499,-6.,335.));
#7944=CARTESIAN_POINT('',(185.231676812499,-6.,335.));
#7945=CARTESIAN_POINT('Origin',(165.231676812499,0.,335.));
#7946=CARTESIAN_POINT('Origin',(175.231676812499,-45.,335.));
#7947=CARTESIAN_POINT('',(185.231676812499,-45.,345.));
#7948=CARTESIAN_POINT('',(165.231676812499,-45.,345.));
#7949=CARTESIAN_POINT('',(185.231676812499,-45.,345.));
#7950=CARTESIAN_POINT('',(165.231676812499,-45.,325.));
#7951=CARTESIAN_POINT('',(165.231676812499,-45.,345.));
#7952=CARTESIAN_POINT('',(185.231676812499,-45.,325.));
#7953=CARTESIAN_POINT('',(165.231676812499,-45.,325.));
#7954=CARTESIAN_POINT('',(185.231676812499,-45.,325.));
#7955=CARTESIAN_POINT('Origin',(165.231676812499,0.,325.));
#7956=CARTESIAN_POINT('',(165.231676812499,45.,345.));
#7957=CARTESIAN_POINT('',(165.231676812499,0.,345.));
#7958=CARTESIAN_POINT('',(165.231676812499,45.,325.));
#7959=CARTESIAN_POINT('',(165.231676812499,45.,345.));
#7960=CARTESIAN_POINT('',(165.231676812499,0.,325.));
#7961=CARTESIAN_POINT('Origin',(185.231676812499,0.,325.));
#7962=CARTESIAN_POINT('',(185.231676812499,45.,325.));
#7963=CARTESIAN_POINT('',(165.231676812499,45.,325.));
#7964=CARTESIAN_POINT('',(185.231676812499,0.,325.));
#7965=CARTESIAN_POINT('Origin',(185.231676812499,0.,345.));
#7966=CARTESIAN_POINT('',(185.231676812499,45.,345.));
#7967=CARTESIAN_POINT('',(185.231676812499,45.,325.));
#7968=CARTESIAN_POINT('',(185.231676812499,0.,345.));
#7969=CARTESIAN_POINT('Origin',(165.231676812499,0.,345.));
#7970=CARTESIAN_POINT('',(185.231676812499,45.,345.));
#7971=CARTESIAN_POINT('Origin',(175.231676812499,45.,335.));
#74509=UNCERTAINTY_MEASURE_WITH_UNIT(LENGTH_MEASURE(0.01),#74524,
'DISTANCE_ACCURACY_VALUE',
'Maximum model space distance between geometric entities at asserted c
onnectivities');
#74512=UNCERTAINTY_MEASURE_WITH_UNIT(LENGTH_MEASURE(0.01),#74524,
'DISTANCE_ACCURACY_VALUE',
'Maximum model space distance between geometric entities at asserted c
onnectivities');
#74520=(
GEOMETRIC_REPRESENTATION_CONTEXT(3)
GLOBAL_UNCERTAINTY_ASSIGNED_CONTEXT((#74509))
GLOBAL_UNIT_ASSIGNED_CONTEXT((#74524,#74526,#74527))
REPRESENTATION_CONTEXT('','3D')
);
#74523=(
GEOMETRIC_REPRESENTATION_CONTEXT(3)
GLOBAL_UNCERTAINTY_ASSIGNED_CONTEXT((#74512))
GLOBAL_UNIT_ASSIGNED_CONTEXT((#74524,#74526,#74527))
REPRESENTATION_CONTEXT('','3D')
);
#74524=(
LENGTH_UNIT()
NAMED_UNIT(*)
SI_UNIT(.MILLI.,.METRE.)
);
#74526=(
NAMED_UNIT(*)
PLANE_ANGLE_UNIT()
SI_UNIT($,.RADIAN.)
);
#74527=(
NAMED_UNIT(*)
SI_UNIT($,.STERADIAN.)
SOLID_ANGLE_UNIT()
);
#74535=SHAPE_DEFINITION_REPRESENTATION(#74545,#74564);
#74545=PRODUCT_DEFINITION_SHAPE('',$,#74575);
#74564=SHAPE_REPRESENTATION('',(#5037),#74520);
#74567=PRODUCT_DEFINITION_CONTEXT('part definition',#74599,'design');
#74575=PRODUCT_DEFINITION('Nut','Nut',#74585,#74567);
#74585=PRODUCT_DEFINITION_FORMATION('',$,#74608);
#74599=APPLICATION_CONTEXT(
'Core Data for Automotive Mechanical Design Process');
#74600=PRODUCT_CONTEXT('part definition',#74599,'mechanical');
#74608=PRODUCT('Nut','Nut',$,(#74600));
#74612=PRESENTATION_STYLE_ASSIGNMENT((#74615));
#74615=SURFACE_STYLE_USAGE(.BOTH.,#74618);
#74618=SURFACE_SIDE_STYLE('',(#74621));
#74621=SURFACE_STYLE_FILL_AREA(#74624);
#74624=FILL_AREA_STYLE('Opaque(215,0,0)',(#74627));
#74627=FILL_AREA_STYLE_COLOUR('Opaque(215,0,0)',#74630);
#74630=COLOUR_RGB('Opaque(215,0,0)', 0.09019608, 0.27058824, 0.51372549);
ENDSEC;
END-ISO-10303-21;
